ISO-10303-21;
HEADER;
FILE_DESCRIPTION((''),'2;1');
FILE_NAME('Washer_1.step','2026-10-09T11:34:15-07:00',(''),(''),'','','');
FILE_SCHEMA (('AUTOMOTIVE_DESIGN { 1 0 10303 214 3 1 1 }'));
ENDSEC;
DATA;
#10=MECHANICAL_DESIGN_GEOMETRIC_PRESENTATION_REPRESENTATION('',(#637),#117170);
#283=ELLIPSE('',#52024,0.281780056072118,0.249999999999999) ;
#284=ELLIPSE('',#52025,0.281780056072094,0.249999999999999) ;
#285=ELLIPSE('',#52032,0.446542271235336,0.249999999999999) ;
#286=ELLIPSE('',#52033,0.446542271235336,0.249999999999999) ;
#287=ELLIPSE('',#52034,0.446542271235316,0.249999999999999) ;
#288=ELLIPSE('',#52035,0.446542271235316,0.249999999999999) ;
#289=ELLIPSE('',#52043,0.281780056072103,0.249999999999999) ;
#290=ELLIPSE('',#52044,0.281780056072118,0.249999999999999) ;
#291=ELLIPSE('',#52053,0.281780056072118,0.249999999999999) ;
#292=ELLIPSE('',#52054,0.281780056072094,0.249999999999999) ;
#293=ELLIPSE('',#52061,0.446542271235316,0.249999999999999) ;
#294=ELLIPSE('',#52062,0.446542271235316,0.249999999999999) ;
#295=ELLIPSE('',#52063,0.446542271235321,0.249999999999999) ;
#296=ELLIPSE('',#52064,0.446542271235321,0.249999999999999) ;
#297=ELLIPSE('',#52073,0.281780056072103,0.249999999999999) ;
#298=ELLIPSE('',#52074,0.281780056072118,0.249999999999999) ;
#299=ELLIPSE('',#52082,0.281780056072103,0.249999999999999) ;
#300=ELLIPSE('',#52083,0.281780056072118,0.249999999999999) ;
#301=ELLIPSE('',#52091,0.446542271235316,0.249999999999999) ;
#302=ELLIPSE('',#52092,0.446542271235316,0.249999999999999) ;
#303=ELLIPSE('',#52093,0.446542271235321,0.249999999999999) ;
#304=ELLIPSE('',#52094,0.446542271235321,0.249999999999999) ;
#305=ELLIPSE('',#52102,0.281780056072118,0.249999999999999) ;
#306=ELLIPSE('',#52103,0.281780056072094,0.249999999999999) ;
#307=ELLIPSE('',#52112,0.281780056072103,0.249999999999999) ;
#308=ELLIPSE('',#52113,0.281780056072118,0.249999999999999) ;
#309=ELLIPSE('',#52120,0.446542271235336,0.249999999999999) ;
#310=ELLIPSE('',#52121,0.446542271235336,0.249999999999999) ;
#311=ELLIPSE('',#52122,0.446542271235316,0.249999999999999) ;
#312=ELLIPSE('',#52123,0.446542271235316,0.249999999999999) ;
#313=ELLIPSE('',#52132,0.281780056072118,0.249999999999999) ;
#314=ELLIPSE('',#52133,0.281780056072094,0.249999999999999) ;
#595=SHAPE_REPRESENTATION_RELATIONSHIP('SRR','None',#117250,#616) ;
#616=ADVANCED_BREP_SHAPE_REPRESENTATION('',(#658),#117158) ;
#637=STYLED_ITEM('',(#117355),#658) ;
#658=MANIFOLD_SOLID_BREP('Body1',#49066) ;
#733=FACE_BOUND('',#15331,.T.) ;
#1991=B_SPLINE_SURFACE_WITH_KNOTS('',3,3,((#87541,#87542,#87543,#87544),
(#87545,#87546,#87547,#87548),(#87549,#87550,#87551,#87552),(#87553,#87554,
#87555,#87556),(#87557,#87558,#87559,#87560)),.UNSPECIFIED.,.F.,.F.,.F.,
(4,1,4),(4,4),(-0.0153229911164263,0.571428571428571,1.01526317510374),
(-1.5707963267949,0.0153229911164264),.UNSPECIFIED.) ;
#1992=B_SPLINE_SURFACE_WITH_KNOTS('',3,3,((#87577,#87578,#87579,#87580,
#87581),(#87582,#87583,#87584,#87585,#87586),(#87587,#87588,#87589,#87590,
#87591),(#87592,#87593,#87594,#87595,#87596),(#87597,#87598,#87599,#87600,
#87601)),.UNSPECIFIED.,.F.,.F.,.F.,(4,1,4),(4,1,4),(-0.00114528587145135,
0.571428571428571,1.00114914004475),(-1.5707963267949,-0.897597901025655,
0.00114914004475158),.UNSPECIFIED.) ;
#1993=B_SPLINE_SURFACE_WITH_KNOTS('',3,3,((#87624,#87625,#87626,#87627),
(#87628,#87629,#87630,#87631),(#87632,#87633,#87634,#87635),(#87636,#87637,
#87638,#87639),(#87640,#87641,#87642,#87643)),.UNSPECIFIED.,.F.,.F.,.F.,
(4,1,4),(4,4),(-0.0153229910814027,0.571428571428571,1.0152631750376),(-1.5707963267949,
0.0153229910814969),.UNSPECIFIED.) ;
#1994=B_SPLINE_SURFACE_WITH_KNOTS('',3,3,((#87665,#87666,#87667,#87668),
(#87669,#87670,#87671,#87672),(#87673,#87674,#87675,#87676),(#87677,#87678,
#87679,#87680),(#87681,#87682,#87683,#87684)),.UNSPECIFIED.,.F.,.F.,.F.,
(4,1,4),(4,4),(-0.0153229913038913,0.571428571428571,1.01526317545535),
(-1.5707963267949,0.0153229913038913),.UNSPECIFIED.) ;
#1995=B_SPLINE_SURFACE_WITH_KNOTS('',3,3,((#87701,#87702,#87703,#87704,
#87705),(#87706,#87707,#87708,#87709,#87710),(#87711,#87712,#87713,#87714,
#87715),(#87716,#87717,#87718,#87719,#87720),(#87721,#87722,#87723,#87724,
#87725)),.UNSPECIFIED.,.F.,.F.,.F.,(4,1,4),(4,1,4),(-0.00114514914518223,
0.571428571428571,1.00114900336214),(-1.5707963267949,-0.897597901025655,
0.0011490033621433),.UNSPECIFIED.) ;
#1996=B_SPLINE_SURFACE_WITH_KNOTS('',3,3,((#87751,#87752,#87753,#87754),
(#87755,#87756,#87757,#87758),(#87759,#87760,#87761,#87762),(#87763,#87764,
#87765,#87766),(#87767,#87768,#87769,#87770)),.UNSPECIFIED.,.F.,.F.,.F.,
(4,1,4),(4,4),(-0.0153229913446253,0.571428571428571,1.01526317558427),
(-1.5707963267949,0.0153229913446253),.UNSPECIFIED.) ;
#1997=B_SPLINE_SURFACE_WITH_KNOTS('',3,3,((#87789,#87790,#87791,#87792),
(#87793,#87794,#87795,#87796),(#87797,#87798,#87799,#87800),(#87801,#87802,
#87803,#87804),(#87805,#87806,#87807,#87808)),.UNSPECIFIED.,.F.,.F.,.F.,
(4,1,4),(4,4),(-0.0153229910815485,0.571428571428571,1.01526317509188),
(-1.5707963267949,0.0153229910815485),.UNSPECIFIED.) ;
#1998=B_SPLINE_SURFACE_WITH_KNOTS('',3,3,((#87828,#87829,#87830,#87831,
#87832),(#87833,#87834,#87835,#87836,#87837),(#87838,#87839,#87840,#87841,
#87842),(#87843,#87844,#87845,#87846,#87847),(#87848,#87849,#87850,#87851,
#87852)),.UNSPECIFIED.,.F.,.F.,.F.,(4,1,4),(4,1,4),(-0.00114539327423229,
0.571428571428571,1.00114924740985),(-1.5707963267949,-0.897597901025655,
0.00114924740985024),.UNSPECIFIED.) ;
#1999=B_SPLINE_SURFACE_WITH_KNOTS('',3,3,((#87875,#87876,#87877,#87878),
(#87879,#87880,#87881,#87882),(#87883,#87884,#87885,#87886),(#87887,#87888,
#87889,#87890),(#87891,#87892,#87893,#87894)),.UNSPECIFIED.,.F.,.F.,.F.,
(4,1,4),(4,4),(-0.0153229911159153,0.571428571428571,1.01526317510136),
(-1.5707963267949,0.0153229911159153),.UNSPECIFIED.) ;
#2000=B_SPLINE_SURFACE_WITH_KNOTS('',3,3,((#87916,#87917,#87918,#87919),
(#87920,#87921,#87922,#87923),(#87924,#87925,#87926,#87927),(#87928,#87929,
#87930,#87931),(#87932,#87933,#87934,#87935)),.UNSPECIFIED.,.F.,.F.,.F.,
(4,1,4),(4,4),(-0.0153229913444723,0.571428571428571,1.01526317558858),
(-1.5707963267949,0.0153229913444723),.UNSPECIFIED.) ;
#2001=B_SPLINE_SURFACE_WITH_KNOTS('',3,3,((#87952,#87953,#87954,#87955,
#87956),(#87957,#87958,#87959,#87960,#87961),(#87962,#87963,#87964,#87965,
#87966),(#87967,#87968,#87969,#87970,#87971),(#87972,#87973,#87974,#87975,
#87976)),.UNSPECIFIED.,.F.,.F.,.F.,(4,1,4),(4,1,4),(-0.00114528587149614,
0.571428571428571,1.00114914004187),(-1.5707963267949,-0.897597901025655,
0.00114914004186756),.UNSPECIFIED.) ;
#2002=B_SPLINE_SURFACE_WITH_KNOTS('',3,3,((#88002,#88003,#88004,#88005),
(#88006,#88007,#88008,#88009),(#88010,#88011,#88012,#88013),(#88014,#88015,
#88016,#88017),(#88018,#88019,#88020,#88021)),.UNSPECIFIED.,.F.,.F.,.F.,
(4,1,4),(4,4),(-0.0153229913034765,0.571428571428571,1.01526317551047),
(-1.5707963267949,0.0153229913034765),.UNSPECIFIED.) ;
#2195=SPHERICAL_SURFACE('',#52027,0.120000000000005) ;
#2196=SPHERICAL_SURFACE('',#52056,0.120000000000005) ;
#2197=SPHERICAL_SURFACE('',#52086,0.120000000000005) ;
#2198=SPHERICAL_SURFACE('',#52115,0.120000000000005) ;
#2486=PLANE('',#52142) ;
#2487=PLANE('',#52143) ;
#2488=PLANE('',#52145) ;
#2489=PLANE('',#52147) ;
#2490=PLANE('',#52149) ;
#2491=PLANE('',#52151) ;
#2492=PLANE('',#52153) ;
#2493=PLANE('',#52162) ;
#2494=PLANE('',#52163) ;
#2495=PLANE('',#52164) ;
#2496=PLANE('',#52165) ;
#2497=PLANE('',#52166) ;
#2498=PLANE('',#52167) ;
#2499=PLANE('',#52177) ;
#2500=PLANE('',#52178) ;
#4271=LINE('',#87568,#7485) ;
#4272=LINE('',#87569,#7486) ;
#4273=LINE('',#87613,#7487) ;
#4274=LINE('',#87614,#7488) ;
#4275=LINE('',#87651,#7489) ;
#4276=LINE('',#87652,#7490) ;
#4277=LINE('',#87654,#7491) ;
#4278=LINE('',#87655,#7492) ;
#4279=LINE('',#87692,#7493) ;
#4280=LINE('',#87693,#7494) ;
#4281=LINE('',#87737,#7495) ;
#4282=LINE('',#87738,#7496) ;
#4283=LINE('',#87740,#7497) ;
#4284=LINE('',#87741,#7498) ;
#4285=LINE('',#87778,#7499) ;
#4286=LINE('',#87779,#7500) ;
#4287=LINE('',#87816,#7501) ;
#4288=LINE('',#87817,#7502) ;
#4289=LINE('',#87819,#7503) ;
#4290=LINE('',#87820,#7504) ;
#4291=LINE('',#87864,#7505) ;
#4292=LINE('',#87865,#7506) ;
#4293=LINE('',#87902,#7507) ;
#4294=LINE('',#87903,#7508) ;
#4295=LINE('',#87905,#7509) ;
#4296=LINE('',#87906,#7510) ;
#4297=LINE('',#87943,#7511) ;
#4298=LINE('',#87944,#7512) ;
#4299=LINE('',#87988,#7513) ;
#4300=LINE('',#87989,#7514) ;
#4301=LINE('',#87991,#7515) ;
#4302=LINE('',#87992,#7516) ;
#4303=LINE('',#88029,#7517) ;
#4304=LINE('',#88030,#7518) ;
#4305=LINE('',#88032,#7519) ;
#4306=LINE('',#88033,#7520) ;
#4307=LINE('',#88035,#7521) ;
#4308=LINE('',#88036,#7522) ;
#4309=LINE('',#88038,#7523) ;
#4310=LINE('',#88039,#7524) ;
#4311=LINE('',#88041,#7525) ;
#4312=LINE('',#88042,#7526) ;
#4313=LINE('',#88044,#7527) ;
#4314=LINE('',#88045,#7528) ;
#4315=LINE('',#88047,#7529) ;
#4316=LINE('',#88048,#7530) ;
#4317=LINE('',#88050,#7531) ;
#4318=LINE('',#88051,#7532) ;
#4319=LINE('',#88053,#7533) ;
#4320=LINE('',#88055,#7534) ;
#4321=LINE('',#88057,#7535) ;
#4322=LINE('',#88059,#7536) ;
#4323=LINE('',#88061,#7537) ;
#4324=LINE('',#88063,#7538) ;
#4325=LINE('',#88065,#7539) ;
#4326=LINE('',#88067,#7540) ;
#4327=LINE('',#88069,#7541) ;
#4328=LINE('',#88071,#7542) ;
#4329=LINE('',#88073,#7543) ;
#4330=LINE('',#88078,#7544) ;
#4331=LINE('',#88079,#7545) ;
#4332=LINE('',#88081,#7546) ;
#4333=LINE('',#88082,#7547) ;
#4334=LINE('',#88084,#7548) ;
#4335=LINE('',#88086,#7549) ;
#4336=LINE('',#88087,#7550) ;
#4337=LINE('',#88089,#7551) ;
#4338=LINE('',#88090,#7552) ;
#4339=LINE('',#88092,#7553) ;
#4340=LINE('',#88093,#7554) ;
#4341=LINE('',#88095,#7555) ;
#4342=LINE('',#88096,#7556) ;
#4343=LINE('',#88109,#7557) ;
#7485=VECTOR('',#61770,10.) ;
#7486=VECTOR('',#61771,10.) ;
#7487=VECTOR('',#61792,10.) ;
#7488=VECTOR('',#61793,10.) ;
#7489=VECTOR('',#61812,10.) ;
#7490=VECTOR('',#61813,10.) ;
#7491=VECTOR('',#61816,10.) ;
#7492=VECTOR('',#61817,10.) ;
#7493=VECTOR('',#61836,10.) ;
#7494=VECTOR('',#61837,10.) ;
#7495=VECTOR('',#61858,10.) ;
#7496=VECTOR('',#61859,10.) ;
#7497=VECTOR('',#61862,10.) ;
#7498=VECTOR('',#61863,10.) ;
#7499=VECTOR('',#61882,10.) ;
#7500=VECTOR('',#61883,10.) ;
#7501=VECTOR('',#61902,10.) ;
#7502=VECTOR('',#61903,10.) ;
#7503=VECTOR('',#61906,10.) ;
#7504=VECTOR('',#61907,10.) ;
#7505=VECTOR('',#61928,10.) ;
#7506=VECTOR('',#61929,10.) ;
#7507=VECTOR('',#61948,10.) ;
#7508=VECTOR('',#61949,10.) ;
#7509=VECTOR('',#61952,10.) ;
#7510=VECTOR('',#61953,10.) ;
#7511=VECTOR('',#61972,10.) ;
#7512=VECTOR('',#61973,10.) ;
#7513=VECTOR('',#61994,10.) ;
#7514=VECTOR('',#61995,10.) ;
#7515=VECTOR('',#61998,10.) ;
#7516=VECTOR('',#61999,10.) ;
#7517=VECTOR('',#62018,10.) ;
#7518=VECTOR('',#62019,10.) ;
#7519=VECTOR('',#62022,10.) ;
#7520=VECTOR('',#62023,10.) ;
#7521=VECTOR('',#62026,10.) ;
#7522=VECTOR('',#62027,10.) ;
#7523=VECTOR('',#62030,10.) ;
#7524=VECTOR('',#62031,10.) ;
#7525=VECTOR('',#62034,10.) ;
#7526=VECTOR('',#62035,10.) ;
#7527=VECTOR('',#62038,10.) ;
#7528=VECTOR('',#62039,10.) ;
#7529=VECTOR('',#62042,10.) ;
#7530=VECTOR('',#62043,10.) ;
#7531=VECTOR('',#62046,10.) ;
#7532=VECTOR('',#62047,10.) ;
#7533=VECTOR('',#62050,10.) ;
#7534=VECTOR('',#62053,10.) ;
#7535=VECTOR('',#62056,10.) ;
#7536=VECTOR('',#62059,10.) ;
#7537=VECTOR('',#62062,10.) ;
#7538=VECTOR('',#62065,10.) ;
#7539=VECTOR('',#62068,10.) ;
#7540=VECTOR('',#62071,10.) ;
#7541=VECTOR('',#62074,10.) ;
#7542=VECTOR('',#62077,10.) ;
#7543=VECTOR('',#62080,10.) ;
#7544=VECTOR('',#62087,10.) ;
#7545=VECTOR('',#62088,10.) ;
#7546=VECTOR('',#62091,10.) ;
#7547=VECTOR('',#62092,10.) ;
#7548=VECTOR('',#62095,10.) ;
#7549=VECTOR('',#62098,10.) ;
#7550=VECTOR('',#62099,10.) ;
#7551=VECTOR('',#62102,10.) ;
#7552=VECTOR('',#62103,10.) ;
#7553=VECTOR('',#62106,10.) ;
#7554=VECTOR('',#62107,10.) ;
#7555=VECTOR('',#62110,10.) ;
#7556=VECTOR('',#62111,10.) ;
#7557=VECTOR('',#62132,1.99999999999999) ;
#9993=CYLINDRICAL_SURFACE('',#52026,0.12) ;
#9994=CYLINDRICAL_SURFACE('',#52036,0.12) ;
#9995=CYLINDRICAL_SURFACE('',#52045,0.12) ;
#9996=CYLINDRICAL_SURFACE('',#52046,0.12) ;
#9997=CYLINDRICAL_SURFACE('',#52055,0.12) ;
#9998=CYLINDRICAL_SURFACE('',#52065,0.12) ;
#9999=CYLINDRICAL_SURFACE('',#52066,0.12) ;
#10000=CYLINDRICAL_SURFACE('',#52075,0.12) ;
#10001=CYLINDRICAL_SURFACE('',#52084,0.12) ;
#10002=CYLINDRICAL_SURFACE('',#52085,0.12) ;
#10003=CYLINDRICAL_SURFACE('',#52095,0.12) ;
#10004=CYLINDRICAL_SURFACE('',#52104,0.12) ;
#10005=CYLINDRICAL_SURFACE('',#52105,0.12) ;
#10006=CYLINDRICAL_SURFACE('',#52114,0.12) ;
#10007=CYLINDRICAL_SURFACE('',#52124,0.12) ;
#10008=CYLINDRICAL_SURFACE('',#52125,0.12) ;
#10009=CYLINDRICAL_SURFACE('',#52134,0.12) ;
#10010=CYLINDRICAL_SURFACE('',#52135,0.12) ;
#10011=CYLINDRICAL_SURFACE('',#52136,0.12) ;
#10012=CYLINDRICAL_SURFACE('',#52137,0.12) ;
#10013=CYLINDRICAL_SURFACE('',#52138,0.12) ;
#10014=CYLINDRICAL_SURFACE('',#52139,0.12) ;
#10015=CYLINDRICAL_SURFACE('',#52140,0.12) ;
#10016=CYLINDRICAL_SURFACE('',#52141,0.12) ;
#10017=CYLINDRICAL_SURFACE('',#52144,0.25) ;
#10018=CYLINDRICAL_SURFACE('',#52146,0.25) ;
#10019=CYLINDRICAL_SURFACE('',#52148,0.25) ;
#10020=CYLINDRICAL_SURFACE('',#52150,0.25) ;
#10021=CYLINDRICAL_SURFACE('',#52152,0.25) ;
#10022=CYLINDRICAL_SURFACE('',#52155,0.25) ;
#10023=CYLINDRICAL_SURFACE('',#52156,0.25) ;
#10024=CYLINDRICAL_SURFACE('',#52157,0.25) ;
#10025=CYLINDRICAL_SURFACE('',#52158,0.25) ;
#10026=CYLINDRICAL_SURFACE('',#52159,0.25) ;
#10027=CYLINDRICAL_SURFACE('',#52160,0.25) ;
#10028=CYLINDRICAL_SURFACE('',#52161,0.25) ;
#10029=CYLINDRICAL_SURFACE('',#52171,1.99999999999999) ;
#12116=FACE_OUTER_BOUND('',#15271,.T.) ;
#12117=FACE_OUTER_BOUND('',#15272,.T.) ;
#12118=FACE_OUTER_BOUND('',#15273,.T.) ;
#12119=FACE_OUTER_BOUND('',#15274,.T.) ;
#12120=FACE_OUTER_BOUND('',#15275,.T.) ;
#12121=FACE_OUTER_BOUND('',#15276,.T.) ;
#12122=FACE_OUTER_BOUND('',#15277,.T.) ;
#12123=FACE_OUTER_BOUND('',#15278,.T.) ;
#12124=FACE_OUTER_BOUND('',#15279,.T.) ;
#12125=FACE_OUTER_BOUND('',#15280,.T.) ;
#12126=FACE_OUTER_BOUND('',#15281,.T.) ;
#12127=FACE_OUTER_BOUND('',#15282,.T.) ;
#12128=FACE_OUTER_BOUND('',#15283,.T.) ;
#12129=FACE_OUTER_BOUND('',#15284,.T.) ;
#12130=FACE_OUTER_BOUND('',#15285,.T.) ;
#12131=FACE_OUTER_BOUND('',#15286,.T.) ;
#12132=FACE_OUTER_BOUND('',#15287,.T.) ;
#12133=FACE_OUTER_BOUND('',#15288,.T.) ;
#12134=FACE_OUTER_BOUND('',#15289,.T.) ;
#12135=FACE_OUTER_BOUND('',#15290,.T.) ;
#12136=FACE_OUTER_BOUND('',#15291,.T.) ;
#12137=FACE_OUTER_BOUND('',#15292,.T.) ;
#12138=FACE_OUTER_BOUND('',#15293,.T.) ;
#12139=FACE_OUTER_BOUND('',#15294,.T.) ;
#12140=FACE_OUTER_BOUND('',#15295,.T.) ;
#12141=FACE_OUTER_BOUND('',#15296,.T.) ;
#12142=FACE_OUTER_BOUND('',#15297,.T.) ;
#12143=FACE_OUTER_BOUND('',#15298,.T.) ;
#12144=FACE_OUTER_BOUND('',#15299,.T.) ;
#12145=FACE_OUTER_BOUND('',#15300,.T.) ;
#12146=FACE_OUTER_BOUND('',#15301,.T.) ;
#12147=FACE_OUTER_BOUND('',#15302,.T.) ;
#12148=FACE_OUTER_BOUND('',#15303,.T.) ;
#12149=FACE_OUTER_BOUND('',#15304,.T.) ;
#12150=FACE_OUTER_BOUND('',#15305,.T.) ;
#12151=FACE_OUTER_BOUND('',#15306,.T.) ;
#12152=FACE_OUTER_BOUND('',#15307,.T.) ;
#12153=FACE_OUTER_BOUND('',#15308,.T.) ;
#12154=FACE_OUTER_BOUND('',#15309,.T.) ;
#12155=FACE_OUTER_BOUND('',#15310,.T.) ;
#12156=FACE_OUTER_BOUND('',#15311,.T.) ;
#12157=FACE_OUTER_BOUND('',#15312,.T.) ;
#12158=FACE_OUTER_BOUND('',#15313,.T.) ;
#12159=FACE_OUTER_BOUND('',#15314,.T.) ;
#12160=FACE_OUTER_BOUND('',#15315,.T.) ;
#12161=FACE_OUTER_BOUND('',#15316,.T.) ;
#12162=FACE_OUTER_BOUND('',#15317,.T.) ;
#12163=FACE_OUTER_BOUND('',#15318,.T.) ;
#12164=FACE_OUTER_BOUND('',#15319,.T.) ;
#12165=FACE_OUTER_BOUND('',#15320,.T.) ;
#12166=FACE_OUTER_BOUND('',#15321,.T.) ;
#12167=FACE_OUTER_BOUND('',#15322,.T.) ;
#12168=FACE_OUTER_BOUND('',#15323,.T.) ;
#12169=FACE_OUTER_BOUND('',#15324,.T.) ;
#12170=FACE_OUTER_BOUND('',#15325,.T.) ;
#12171=FACE_OUTER_BOUND('',#15326,.T.) ;
#12172=FACE_OUTER_BOUND('',#15327,.T.) ;
#12173=FACE_OUTER_BOUND('',#15328,.T.) ;
#12174=FACE_OUTER_BOUND('',#15329,.T.) ;
#12175=FACE_OUTER_BOUND('',#15330,.T.) ;
#12176=FACE_OUTER_BOUND('',#15332,.T.) ;
#12177=FACE_OUTER_BOUND('',#15333,.T.) ;
#12178=FACE_OUTER_BOUND('',#15334,.T.) ;
#12179=FACE_OUTER_BOUND('',#15335,.T.) ;
#12180=FACE_OUTER_BOUND('',#15336,.T.) ;
#12181=FACE_OUTER_BOUND('',#15337,.T.) ;
#12182=FACE_OUTER_BOUND('',#15338,.T.) ;
#12183=FACE_OUTER_BOUND('',#15339,.T.) ;
#12184=FACE_OUTER_BOUND('',#15340,.T.) ;
#12185=FACE_OUTER_BOUND('',#15341,.T.) ;
#12186=FACE_OUTER_BOUND('',#15342,.T.) ;
#12187=FACE_OUTER_BOUND('',#15343,.T.) ;
#12188=FACE_OUTER_BOUND('',#15344,.T.) ;
#12189=FACE_OUTER_BOUND('',#15345,.T.) ;
#12190=FACE_OUTER_BOUND('',#15346,.T.) ;
#12191=FACE_OUTER_BOUND('',#15347,.T.) ;
#12192=FACE_OUTER_BOUND('',#15348,.T.) ;
#12193=FACE_OUTER_BOUND('',#15349,.T.) ;
#15271=EDGE_LOOP('',(#37326,#37327,#37328,#37329)) ;
#15272=EDGE_LOOP('',(#37330,#37331,#37332)) ;
#15273=EDGE_LOOP('',(#37333,#37334,#37335,#37336)) ;
#15274=EDGE_LOOP('',(#37337,#37338,#37339)) ;
#15275=EDGE_LOOP('',(#37340,#37341,#37342,#37343,#37344)) ;
#15276=EDGE_LOOP('',(#37345,#37346,#37347,#37348)) ;
#15277=EDGE_LOOP('',(#37349,#37350,#37351,#37352)) ;
#15278=EDGE_LOOP('',(#37353,#37354,#37355)) ;
#15279=EDGE_LOOP('',(#37356,#37357,#37358,#37359)) ;
#15280=EDGE_LOOP('',(#37360,#37361,#37362,#37363)) ;
#15281=EDGE_LOOP('',(#37364,#37365,#37366,#37367)) ;
#15282=EDGE_LOOP('',(#37368,#37369,#37370)) ;
#15283=EDGE_LOOP('',(#37371,#37372,#37373,#37374)) ;
#15284=EDGE_LOOP('',(#37375,#37376,#37377)) ;
#15285=EDGE_LOOP('',(#37378,#37379,#37380,#37381,#37382)) ;
#15286=EDGE_LOOP('',(#37383,#37384,#37385,#37386)) ;
#15287=EDGE_LOOP('',(#37387,#37388,#37389,#37390)) ;
#15288=EDGE_LOOP('',(#37391,#37392,#37393,#37394)) ;
#15289=EDGE_LOOP('',(#37395,#37396,#37397)) ;
#15290=EDGE_LOOP('',(#37398,#37399,#37400,#37401)) ;
#15291=EDGE_LOOP('',(#37402,#37403,#37404,#37405)) ;
#15292=EDGE_LOOP('',(#37406,#37407,#37408)) ;
#15293=EDGE_LOOP('',(#37409,#37410,#37411,#37412)) ;
#15294=EDGE_LOOP('',(#37413,#37414,#37415,#37416)) ;
#15295=EDGE_LOOP('',(#37417,#37418,#37419)) ;
#15296=EDGE_LOOP('',(#37420,#37421,#37422,#37423,#37424)) ;
#15297=EDGE_LOOP('',(#37425,#37426,#37427,#37428)) ;
#15298=EDGE_LOOP('',(#37429,#37430,#37431,#37432)) ;
#15299=EDGE_LOOP('',(#37433,#37434,#37435)) ;
#15300=EDGE_LOOP('',(#37436,#37437,#37438,#37439)) ;
#15301=EDGE_LOOP('',(#37440,#37441,#37442,#37443)) ;
#15302=EDGE_LOOP('',(#37444,#37445,#37446,#37447)) ;
#15303=EDGE_LOOP('',(#37448,#37449,#37450)) ;
#15304=EDGE_LOOP('',(#37451,#37452,#37453,#37454)) ;
#15305=EDGE_LOOP('',(#37455,#37456,#37457)) ;
#15306=EDGE_LOOP('',(#37458,#37459,#37460,#37461,#37462)) ;
#15307=EDGE_LOOP('',(#37463,#37464,#37465,#37466)) ;
#15308=EDGE_LOOP('',(#37467,#37468,#37469,#37470)) ;
#15309=EDGE_LOOP('',(#37471,#37472,#37473,#37474)) ;
#15310=EDGE_LOOP('',(#37475,#37476,#37477)) ;
#15311=EDGE_LOOP('',(#37478,#37479,#37480,#37481)) ;
#15312=EDGE_LOOP('',(#37482,#37483,#37484,#37485)) ;
#15313=EDGE_LOOP('',(#37486,#37487,#37488,#37489)) ;
#15314=EDGE_LOOP('',(#37490,#37491,#37492,#37493)) ;
#15315=EDGE_LOOP('',(#37494,#37495,#37496,#37497)) ;
#15316=EDGE_LOOP('',(#37498,#37499,#37500,#37501)) ;
#15317=EDGE_LOOP('',(#37502,#37503,#37504,#37505)) ;
#15318=EDGE_LOOP('',(#37506,#37507,#37508,#37509)) ;
#15319=EDGE_LOOP('',(#37510,#37511,#37512,#37513)) ;
#15320=EDGE_LOOP('',(#37514,#37515,#37516,#37517)) ;
#15321=EDGE_LOOP('',(#37518,#37519,#37520,#37521,#37522)) ;
#15322=EDGE_LOOP('',(#37523,#37524,#37525,#37526)) ;
#15323=EDGE_LOOP('',(#37527,#37528,#37529,#37530,#37531)) ;
#15324=EDGE_LOOP('',(#37532,#37533,#37534,#37535)) ;
#15325=EDGE_LOOP('',(#37536,#37537,#37538,#37539)) ;
#15326=EDGE_LOOP('',(#37540,#37541,#37542,#37543)) ;
#15327=EDGE_LOOP('',(#37544,#37545,#37546,#37547,#37548)) ;
#15328=EDGE_LOOP('',(#37549,#37550,#37551,#37552)) ;
#15329=EDGE_LOOP('',(#37553,#37554,#37555,#37556,#37557)) ;
#15330=EDGE_LOOP('',(#37558)) ;
#15331=EDGE_LOOP('',(#37559,#37560,#37561,#37562,#37563,#37564,#37565,#37566,
#37567,#37568,#37569,#37570,#37571,#37572,#37573,#37574,#37575,#37576,#37577,
#37578)) ;
#15332=EDGE_LOOP('',(#37579,#37580,#37581,#37582,#37583)) ;
#15333=EDGE_LOOP('',(#37584,#37585,#37586,#37587)) ;
#15334=EDGE_LOOP('',(#37588,#37589,#37590,#37591)) ;
#15335=EDGE_LOOP('',(#37592,#37593,#37594,#37595,#37596)) ;
#15336=EDGE_LOOP('',(#37597,#37598,#37599,#37600,#37601)) ;
#15337=EDGE_LOOP('',(#37602,#37603,#37604,#37605)) ;
#15338=EDGE_LOOP('',(#37606,#37607,#37608,#37609,#37610)) ;
#15339=EDGE_LOOP('',(#37611,#37612,#37613,#37614)) ;
#15340=EDGE_LOOP('',(#37615,#37616,#37617,#37618)) ;
#15341=EDGE_LOOP('',(#37619,#37620,#37621,#37622)) ;
#15342=EDGE_LOOP('',(#37623,#37624,#37625,#37626)) ;
#15343=EDGE_LOOP('',(#37627,#37628,#37629,#37630)) ;
#15344=EDGE_LOOP('',(#37631,#37632,#37633,#37634,#37635,#37636,#37637,#37638,
#37639,#37640,#37641,#37642)) ;
#15345=EDGE_LOOP('',(#37643,#37644,#37645,#37646)) ;
#15346=EDGE_LOOP('',(#37647,#37648,#37649,#37650,#37651)) ;
#15347=EDGE_LOOP('',(#37652,#37653,#37654,#37655,#37656)) ;
#15348=EDGE_LOOP('',(#37657)) ;
#15349=EDGE_LOOP('',(#37658,#37659,#37660,#37661)) ;
#18406=CIRCLE('',#52019,0.120000000000005) ;
#18407=CIRCLE('',#52020,0.120000000000005) ;
#18408=CIRCLE('',#52021,0.12) ;
#18409=CIRCLE('',#52022,0.240000000000009) ;
#18410=CIRCLE('',#52023,0.119999999999969) ;
#18411=CIRCLE('',#52028,0.120000000000005) ;
#18412=CIRCLE('',#52029,0.120000000000005) ;
#18413=CIRCLE('',#52030,0.12) ;
#18414=CIRCLE('',#52031,0.120000000000022) ;
#18415=CIRCLE('',#52038,0.120000000000005) ;
#18416=CIRCLE('',#52039,0.120000000000005) ;
#18417=CIRCLE('',#52040,0.12) ;
#18418=CIRCLE('',#52041,0.240000000000009) ;
#18419=CIRCLE('',#52042,0.119999999999987) ;
#18420=CIRCLE('',#52048,0.120000000000005) ;
#18421=CIRCLE('',#52049,0.120000000000005) ;
#18422=CIRCLE('',#52050,0.12) ;
#18423=CIRCLE('',#52051,0.240000000000009) ;
#18424=CIRCLE('',#52052,0.119999999999969) ;
#18425=CIRCLE('',#52057,0.120000000000005) ;
#18426=CIRCLE('',#52058,0.120000000000005) ;
#18427=CIRCLE('',#52059,0.12) ;
#18428=CIRCLE('',#52060,0.120000000000005) ;
#18429=CIRCLE('',#52068,0.120000000000005) ;
#18430=CIRCLE('',#52069,0.120000000000005) ;
#18431=CIRCLE('',#52070,0.12) ;
#18432=CIRCLE('',#52071,0.240000000000009) ;
#18433=CIRCLE('',#52072,0.119999999999987) ;
#18434=CIRCLE('',#52077,0.120000000000005) ;
#18435=CIRCLE('',#52078,0.120000000000005) ;
#18436=CIRCLE('',#52079,0.12) ;
#18437=CIRCLE('',#52080,0.240000000000009) ;
#18438=CIRCLE('',#52081,0.119999999999987) ;
#18439=CIRCLE('',#52087,0.120000000000005) ;
#18440=CIRCLE('',#52088,0.120000000000005) ;
#18441=CIRCLE('',#52089,0.12) ;
#18442=CIRCLE('',#52090,0.120000000000005) ;
#18443=CIRCLE('',#52097,0.120000000000005) ;
#18444=CIRCLE('',#52098,0.120000000000005) ;
#18445=CIRCLE('',#52099,0.12) ;
#18446=CIRCLE('',#52100,0.240000000000009) ;
#18447=CIRCLE('',#52101,0.119999999999969) ;
#18448=CIRCLE('',#52107,0.120000000000005) ;
#18449=CIRCLE('',#52108,0.119999999999996) ;
#18450=CIRCLE('',#52109,0.12) ;
#18451=CIRCLE('',#52110,0.239999999999991) ;
#18452=CIRCLE('',#52111,0.119999999999987) ;
#18453=CIRCLE('',#52116,0.120000000000005) ;
#18454=CIRCLE('',#52117,0.120000000000005) ;
#18455=CIRCLE('',#52118,0.12) ;
#18456=CIRCLE('',#52119,0.120000000000022) ;
#18457=CIRCLE('',#52127,0.119999999999996) ;
#18458=CIRCLE('',#52128,0.120000000000005) ;
#18459=CIRCLE('',#52129,0.12) ;
#18460=CIRCLE('',#52130,0.240000000000009) ;
#18461=CIRCLE('',#52131,0.119999999999969) ;
#18462=CIRCLE('',#52154,1.74999999999999) ;
#18463=CIRCLE('',#52169,0.25) ;
#18464=CIRCLE('',#52170,1.99999999999999) ;
#18465=CIRCLE('',#52172,1.99999999999999) ;
#18466=CIRCLE('',#52173,1.99999999999999) ;
#18467=CIRCLE('',#52175,1.74999999999999) ;
#18468=CIRCLE('',#52176,0.25) ;
#21393=VERTEX_POINT('',#87533) ;
#21394=VERTEX_POINT('',#87534) ;
#21395=VERTEX_POINT('',#87536) ;
#21396=VERTEX_POINT('',#87538) ;
#21397=VERTEX_POINT('',#87561) ;
#21398=VERTEX_POINT('',#87562) ;
#21399=VERTEX_POINT('',#87564) ;
#21400=VERTEX_POINT('',#87571) ;
#21401=VERTEX_POINT('',#87572) ;
#21402=VERTEX_POINT('',#87574) ;
#21403=VERTEX_POINT('',#87602) ;
#21404=VERTEX_POINT('',#87603) ;
#21405=VERTEX_POINT('',#87605) ;
#21406=VERTEX_POINT('',#87607) ;
#21407=VERTEX_POINT('',#87609) ;
#21408=VERTEX_POINT('',#87616) ;
#21409=VERTEX_POINT('',#87617) ;
#21410=VERTEX_POINT('',#87619) ;
#21411=VERTEX_POINT('',#87621) ;
#21412=VERTEX_POINT('',#87644) ;
#21413=VERTEX_POINT('',#87645) ;
#21414=VERTEX_POINT('',#87647) ;
#21415=VERTEX_POINT('',#87657) ;
#21416=VERTEX_POINT('',#87658) ;
#21417=VERTEX_POINT('',#87660) ;
#21418=VERTEX_POINT('',#87662) ;
#21419=VERTEX_POINT('',#87685) ;
#21420=VERTEX_POINT('',#87686) ;
#21421=VERTEX_POINT('',#87688) ;
#21422=VERTEX_POINT('',#87695) ;
#21423=VERTEX_POINT('',#87696) ;
#21424=VERTEX_POINT('',#87698) ;
#21425=VERTEX_POINT('',#87726) ;
#21426=VERTEX_POINT('',#87727) ;
#21427=VERTEX_POINT('',#87729) ;
#21428=VERTEX_POINT('',#87731) ;
#21429=VERTEX_POINT('',#87733) ;
#21430=VERTEX_POINT('',#87743) ;
#21431=VERTEX_POINT('',#87744) ;
#21432=VERTEX_POINT('',#87746) ;
#21433=VERTEX_POINT('',#87748) ;
#21434=VERTEX_POINT('',#87771) ;
#21435=VERTEX_POINT('',#87772) ;
#21436=VERTEX_POINT('',#87774) ;
#21437=VERTEX_POINT('',#87781) ;
#21438=VERTEX_POINT('',#87782) ;
#21439=VERTEX_POINT('',#87784) ;
#21440=VERTEX_POINT('',#87786) ;
#21441=VERTEX_POINT('',#87809) ;
#21442=VERTEX_POINT('',#87810) ;
#21443=VERTEX_POINT('',#87812) ;
#21444=VERTEX_POINT('',#87822) ;
#21445=VERTEX_POINT('',#87823) ;
#21446=VERTEX_POINT('',#87825) ;
#21447=VERTEX_POINT('',#87853) ;
#21448=VERTEX_POINT('',#87854) ;
#21449=VERTEX_POINT('',#87856) ;
#21450=VERTEX_POINT('',#87858) ;
#21451=VERTEX_POINT('',#87860) ;
#21452=VERTEX_POINT('',#87867) ;
#21453=VERTEX_POINT('',#87868) ;
#21454=VERTEX_POINT('',#87870) ;
#21455=VERTEX_POINT('',#87872) ;
#21456=VERTEX_POINT('',#87895) ;
#21457=VERTEX_POINT('',#87896) ;
#21458=VERTEX_POINT('',#87898) ;
#21459=VERTEX_POINT('',#87908) ;
#21460=VERTEX_POINT('',#87909) ;
#21461=VERTEX_POINT('',#87911) ;
#21462=VERTEX_POINT('',#87913) ;
#21463=VERTEX_POINT('',#87936) ;
#21464=VERTEX_POINT('',#87937) ;
#21465=VERTEX_POINT('',#87939) ;
#21466=VERTEX_POINT('',#87946) ;
#21467=VERTEX_POINT('',#87947) ;
#21468=VERTEX_POINT('',#87949) ;
#21469=VERTEX_POINT('',#87977) ;
#21470=VERTEX_POINT('',#87978) ;
#21471=VERTEX_POINT('',#87980) ;
#21472=VERTEX_POINT('',#87982) ;
#21473=VERTEX_POINT('',#87984) ;
#21474=VERTEX_POINT('',#87994) ;
#21475=VERTEX_POINT('',#87995) ;
#21476=VERTEX_POINT('',#87997) ;
#21477=VERTEX_POINT('',#87999) ;
#21478=VERTEX_POINT('',#88022) ;
#21479=VERTEX_POINT('',#88023) ;
#21480=VERTEX_POINT('',#88025) ;
#21481=VERTEX_POINT('',#88075) ;
#21482=VERTEX_POINT('',#88104) ;
#21483=VERTEX_POINT('',#88108) ;
#21484=VERTEX_POINT('',#88110) ;
#21485=VERTEX_POINT('',#88114) ;
#26941=EDGE_CURVE('',#21393,#21394,#18406,.T.) ;
#26942=EDGE_CURVE('',#21395,#21393,#18407,.F.) ;
#26943=EDGE_CURVE('',#21396,#21395,#18408,.T.) ;
#26944=EDGE_CURVE('',#21396,#21394,#18409,.T.) ;
#26945=EDGE_CURVE('',#21397,#21398,#18410,.T.) ;
#26946=EDGE_CURVE('',#21398,#21399,#283,.T.) ;
#26947=EDGE_CURVE('',#21399,#21397,#284,.T.) ;
#26948=EDGE_CURVE('',#21397,#21395,#4271,.T.) ;
#26949=EDGE_CURVE('',#21393,#21398,#4272,.T.) ;
#26950=EDGE_CURVE('',#21400,#21401,#18411,.F.) ;
#26951=EDGE_CURVE('',#21402,#21400,#18412,.F.) ;
#26952=EDGE_CURVE('',#21401,#21402,#18413,.F.) ;
#26953=EDGE_CURVE('',#21403,#21404,#18414,.T.) ;
#26954=EDGE_CURVE('',#21404,#21405,#285,.T.) ;
#26955=EDGE_CURVE('',#21405,#21406,#286,.T.) ;
#26956=EDGE_CURVE('',#21406,#21407,#287,.T.) ;
#26957=EDGE_CURVE('',#21407,#21403,#288,.T.) ;
#26958=EDGE_CURVE('',#21403,#21402,#4273,.T.) ;
#26959=EDGE_CURVE('',#21400,#21404,#4274,.T.) ;
#26960=EDGE_CURVE('',#21408,#21409,#18415,.T.) ;
#26961=EDGE_CURVE('',#21410,#21408,#18416,.F.) ;
#26962=EDGE_CURVE('',#21411,#21410,#18417,.T.) ;
#26963=EDGE_CURVE('',#21411,#21409,#18418,.T.) ;
#26964=EDGE_CURVE('',#21412,#21413,#18419,.T.) ;
#26965=EDGE_CURVE('',#21413,#21414,#289,.T.) ;
#26966=EDGE_CURVE('',#21414,#21412,#290,.T.) ;
#26967=EDGE_CURVE('',#21412,#21410,#4275,.T.) ;
#26968=EDGE_CURVE('',#21408,#21413,#4276,.T.) ;
#26969=EDGE_CURVE('',#21394,#21411,#4277,.T.) ;
#26970=EDGE_CURVE('',#21410,#21393,#4278,.T.) ;
#26971=EDGE_CURVE('',#21415,#21416,#18420,.T.) ;
#26972=EDGE_CURVE('',#21417,#21415,#18421,.F.) ;
#26973=EDGE_CURVE('',#21418,#21417,#18422,.T.) ;
#26974=EDGE_CURVE('',#21418,#21416,#18423,.T.) ;
#26975=EDGE_CURVE('',#21419,#21420,#18424,.T.) ;
#26976=EDGE_CURVE('',#21420,#21421,#291,.T.) ;
#26977=EDGE_CURVE('',#21421,#21419,#292,.T.) ;
#26978=EDGE_CURVE('',#21419,#21417,#4279,.T.) ;
#26979=EDGE_CURVE('',#21415,#21420,#4280,.T.) ;
#26980=EDGE_CURVE('',#21422,#21423,#18425,.F.) ;
#26981=EDGE_CURVE('',#21424,#21422,#18426,.F.) ;
#26982=EDGE_CURVE('',#21423,#21424,#18427,.F.) ;
#26983=EDGE_CURVE('',#21425,#21426,#18428,.T.) ;
#26984=EDGE_CURVE('',#21426,#21427,#293,.T.) ;
#26985=EDGE_CURVE('',#21427,#21428,#294,.T.) ;
#26986=EDGE_CURVE('',#21428,#21429,#295,.T.) ;
#26987=EDGE_CURVE('',#21429,#21425,#296,.T.) ;
#26988=EDGE_CURVE('',#21425,#21424,#4281,.T.) ;
#26989=EDGE_CURVE('',#21422,#21426,#4282,.T.) ;
#26990=EDGE_CURVE('',#21409,#21423,#4283,.T.) ;
#26991=EDGE_CURVE('',#21424,#21408,#4284,.T.) ;
#26992=EDGE_CURVE('',#21430,#21431,#18429,.T.) ;
#26993=EDGE_CURVE('',#21432,#21430,#18430,.F.) ;
#26994=EDGE_CURVE('',#21433,#21432,#18431,.T.) ;
#26995=EDGE_CURVE('',#21433,#21431,#18432,.T.) ;
#26996=EDGE_CURVE('',#21434,#21435,#18433,.T.) ;
#26997=EDGE_CURVE('',#21435,#21436,#297,.T.) ;
#26998=EDGE_CURVE('',#21436,#21434,#298,.T.) ;
#26999=EDGE_CURVE('',#21434,#21432,#4285,.T.) ;
#27000=EDGE_CURVE('',#21430,#21435,#4286,.T.) ;
#27001=EDGE_CURVE('',#21437,#21438,#18434,.T.) ;
#27002=EDGE_CURVE('',#21439,#21437,#18435,.F.) ;
#27003=EDGE_CURVE('',#21440,#21439,#18436,.T.) ;
#27004=EDGE_CURVE('',#21440,#21438,#18437,.T.) ;
#27005=EDGE_CURVE('',#21441,#21442,#18438,.T.) ;
#27006=EDGE_CURVE('',#21442,#21443,#299,.T.) ;
#27007=EDGE_CURVE('',#21443,#21441,#300,.T.) ;
#27008=EDGE_CURVE('',#21441,#21439,#4287,.T.) ;
#27009=EDGE_CURVE('',#21437,#21442,#4288,.T.) ;
#27010=EDGE_CURVE('',#21423,#21440,#4289,.T.) ;
#27011=EDGE_CURVE('',#21439,#21422,#4290,.T.) ;
#27012=EDGE_CURVE('',#21444,#21445,#18439,.F.) ;
#27013=EDGE_CURVE('',#21446,#21444,#18440,.F.) ;
#27014=EDGE_CURVE('',#21445,#21446,#18441,.F.) ;
#27015=EDGE_CURVE('',#21447,#21448,#18442,.T.) ;
#27016=EDGE_CURVE('',#21448,#21449,#301,.T.) ;
#27017=EDGE_CURVE('',#21449,#21450,#302,.T.) ;
#27018=EDGE_CURVE('',#21450,#21451,#303,.T.) ;
#27019=EDGE_CURVE('',#21451,#21447,#304,.T.) ;
#27020=EDGE_CURVE('',#21447,#21446,#4291,.T.) ;
#27021=EDGE_CURVE('',#21444,#21448,#4292,.T.) ;
#27022=EDGE_CURVE('',#21452,#21453,#18443,.T.) ;
#27023=EDGE_CURVE('',#21454,#21452,#18444,.F.) ;
#27024=EDGE_CURVE('',#21455,#21454,#18445,.T.) ;
#27025=EDGE_CURVE('',#21455,#21453,#18446,.T.) ;
#27026=EDGE_CURVE('',#21456,#21457,#18447,.T.) ;
#27027=EDGE_CURVE('',#21457,#21458,#305,.T.) ;
#27028=EDGE_CURVE('',#21458,#21456,#306,.T.) ;
#27029=EDGE_CURVE('',#21456,#21454,#4293,.T.) ;
#27030=EDGE_CURVE('',#21452,#21457,#4294,.T.) ;
#27031=EDGE_CURVE('',#21438,#21455,#4295,.T.) ;
#27032=EDGE_CURVE('',#21454,#21437,#4296,.T.) ;
#27033=EDGE_CURVE('',#21459,#21460,#18448,.T.) ;
#27034=EDGE_CURVE('',#21461,#21459,#18449,.F.) ;
#27035=EDGE_CURVE('',#21462,#21461,#18450,.T.) ;
#27036=EDGE_CURVE('',#21462,#21460,#18451,.T.) ;
#27037=EDGE_CURVE('',#21463,#21464,#18452,.T.) ;
#27038=EDGE_CURVE('',#21464,#21465,#307,.T.) ;
#27039=EDGE_CURVE('',#21465,#21463,#308,.T.) ;
#27040=EDGE_CURVE('',#21463,#21461,#4297,.T.) ;
#27041=EDGE_CURVE('',#21459,#21464,#4298,.T.) ;
#27042=EDGE_CURVE('',#21466,#21467,#18453,.F.) ;
#27043=EDGE_CURVE('',#21468,#21466,#18454,.F.) ;
#27044=EDGE_CURVE('',#21467,#21468,#18455,.F.) ;
#27045=EDGE_CURVE('',#21469,#21470,#18456,.T.) ;
#27046=EDGE_CURVE('',#21470,#21471,#309,.T.) ;
#27047=EDGE_CURVE('',#21471,#21472,#310,.T.) ;
#27048=EDGE_CURVE('',#21472,#21473,#311,.T.) ;
#27049=EDGE_CURVE('',#21473,#21469,#312,.T.) ;
#27050=EDGE_CURVE('',#21469,#21468,#4299,.T.) ;
#27051=EDGE_CURVE('',#21466,#21470,#4300,.T.) ;
#27052=EDGE_CURVE('',#21453,#21467,#4301,.T.) ;
#27053=EDGE_CURVE('',#21468,#21452,#4302,.T.) ;
#27054=EDGE_CURVE('',#21474,#21475,#18457,.T.) ;
#27055=EDGE_CURVE('',#21476,#21474,#18458,.F.) ;
#27056=EDGE_CURVE('',#21477,#21476,#18459,.T.) ;
#27057=EDGE_CURVE('',#21477,#21475,#18460,.T.) ;
#27058=EDGE_CURVE('',#21478,#21479,#18461,.T.) ;
#27059=EDGE_CURVE('',#21479,#21480,#313,.T.) ;
#27060=EDGE_CURVE('',#21480,#21478,#314,.T.) ;
#27061=EDGE_CURVE('',#21478,#21476,#4303,.T.) ;
#27062=EDGE_CURVE('',#21474,#21479,#4304,.T.) ;
#27063=EDGE_CURVE('',#21467,#21477,#4305,.T.) ;
#27064=EDGE_CURVE('',#21476,#21466,#4306,.T.) ;
#27065=EDGE_CURVE('',#21475,#21462,#4307,.T.) ;
#27066=EDGE_CURVE('',#21461,#21474,#4308,.T.) ;
#27067=EDGE_CURVE('',#21460,#21445,#4309,.T.) ;
#27068=EDGE_CURVE('',#21446,#21459,#4310,.T.) ;
#27069=EDGE_CURVE('',#21445,#21433,#4311,.T.) ;
#27070=EDGE_CURVE('',#21432,#21444,#4312,.T.) ;
#27071=EDGE_CURVE('',#21431,#21418,#4313,.T.) ;
#27072=EDGE_CURVE('',#21417,#21430,#4314,.T.) ;
#27073=EDGE_CURVE('',#21416,#21401,#4315,.T.) ;
#27074=EDGE_CURVE('',#21402,#21415,#4316,.T.) ;
#27075=EDGE_CURVE('',#21401,#21396,#4317,.T.) ;
#27076=EDGE_CURVE('',#21395,#21400,#4318,.T.) ;
#27077=EDGE_CURVE('',#21398,#21412,#4319,.T.) ;
#27078=EDGE_CURVE('',#21413,#21425,#4320,.T.) ;
#27079=EDGE_CURVE('',#21428,#21414,#4321,.T.) ;
#27080=EDGE_CURVE('',#21426,#21441,#4322,.T.) ;
#27081=EDGE_CURVE('',#21443,#21428,#4323,.T.) ;
#27082=EDGE_CURVE('',#21442,#21456,#4324,.T.) ;
#27083=EDGE_CURVE('',#21458,#21443,#4325,.T.) ;
#27084=EDGE_CURVE('',#21457,#21469,#4326,.T.) ;
#27085=EDGE_CURVE('',#21472,#21458,#4327,.T.) ;
#27086=EDGE_CURVE('',#21470,#21478,#4328,.T.) ;
#27087=EDGE_CURVE('',#21480,#21472,#4329,.T.) ;
#27088=EDGE_CURVE('',#21481,#21481,#18462,.T.) ;
#27089=EDGE_CURVE('',#21450,#21465,#4330,.T.) ;
#27090=EDGE_CURVE('',#21464,#21447,#4331,.T.) ;
#27091=EDGE_CURVE('',#21465,#21480,#4332,.T.) ;
#27092=EDGE_CURVE('',#21479,#21463,#4333,.T.) ;
#27093=EDGE_CURVE('',#21414,#21399,#4334,.T.) ;
#27094=EDGE_CURVE('',#21399,#21406,#4335,.T.) ;
#27095=EDGE_CURVE('',#21404,#21397,#4336,.T.) ;
#27096=EDGE_CURVE('',#21406,#21421,#4337,.T.) ;
#27097=EDGE_CURVE('',#21420,#21403,#4338,.T.) ;
#27098=EDGE_CURVE('',#21421,#21436,#4339,.T.) ;
#27099=EDGE_CURVE('',#21435,#21419,#4340,.T.) ;
#27100=EDGE_CURVE('',#21436,#21450,#4341,.T.) ;
#27101=EDGE_CURVE('',#21448,#21434,#4342,.T.) ;
#27102=EDGE_CURVE('',#21481,#21482,#18463,.T.) ;
#27103=EDGE_CURVE('',#21482,#21482,#18464,.T.) ;
#27104=EDGE_CURVE('',#21482,#21483,#4343,.T.) ;
#27105=EDGE_CURVE('',#21484,#21483,#18465,.T.) ;
#27106=EDGE_CURVE('',#21483,#21484,#18466,.T.) ;
#27107=EDGE_CURVE('',#21485,#21485,#18467,.T.) ;
#27108=EDGE_CURVE('',#21485,#21484,#18468,.T.) ;
#37326=ORIENTED_EDGE('',*,*,#26941,.F.) ;
#37327=ORIENTED_EDGE('',*,*,#26942,.F.) ;
#37328=ORIENTED_EDGE('',*,*,#26943,.F.) ;
#37329=ORIENTED_EDGE('',*,*,#26944,.T.) ;
#37330=ORIENTED_EDGE('',*,*,#26945,.T.) ;
#37331=ORIENTED_EDGE('',*,*,#26946,.T.) ;
#37332=ORIENTED_EDGE('',*,*,#26947,.T.) ;
#37333=ORIENTED_EDGE('',*,*,#26945,.F.) ;
#37334=ORIENTED_EDGE('',*,*,#26948,.T.) ;
#37335=ORIENTED_EDGE('',*,*,#26942,.T.) ;
#37336=ORIENTED_EDGE('',*,*,#26949,.T.) ;
#37337=ORIENTED_EDGE('',*,*,#26950,.F.) ;
#37338=ORIENTED_EDGE('',*,*,#26951,.F.) ;
#37339=ORIENTED_EDGE('',*,*,#26952,.F.) ;
#37340=ORIENTED_EDGE('',*,*,#26953,.T.) ;
#37341=ORIENTED_EDGE('',*,*,#26954,.T.) ;
#37342=ORIENTED_EDGE('',*,*,#26955,.T.) ;
#37343=ORIENTED_EDGE('',*,*,#26956,.T.) ;
#37344=ORIENTED_EDGE('',*,*,#26957,.T.) ;
#37345=ORIENTED_EDGE('',*,*,#26953,.F.) ;
#37346=ORIENTED_EDGE('',*,*,#26958,.T.) ;
#37347=ORIENTED_EDGE('',*,*,#26951,.T.) ;
#37348=ORIENTED_EDGE('',*,*,#26959,.T.) ;
#37349=ORIENTED_EDGE('',*,*,#26960,.F.) ;
#37350=ORIENTED_EDGE('',*,*,#26961,.F.) ;
#37351=ORIENTED_EDGE('',*,*,#26962,.F.) ;
#37352=ORIENTED_EDGE('',*,*,#26963,.T.) ;
#37353=ORIENTED_EDGE('',*,*,#26964,.T.) ;
#37354=ORIENTED_EDGE('',*,*,#26965,.T.) ;
#37355=ORIENTED_EDGE('',*,*,#26966,.T.) ;
#37356=ORIENTED_EDGE('',*,*,#26964,.F.) ;
#37357=ORIENTED_EDGE('',*,*,#26967,.T.) ;
#37358=ORIENTED_EDGE('',*,*,#26961,.T.) ;
#37359=ORIENTED_EDGE('',*,*,#26968,.T.) ;
#37360=ORIENTED_EDGE('',*,*,#26941,.T.) ;
#37361=ORIENTED_EDGE('',*,*,#26969,.T.) ;
#37362=ORIENTED_EDGE('',*,*,#26962,.T.) ;
#37363=ORIENTED_EDGE('',*,*,#26970,.T.) ;
#37364=ORIENTED_EDGE('',*,*,#26971,.F.) ;
#37365=ORIENTED_EDGE('',*,*,#26972,.F.) ;
#37366=ORIENTED_EDGE('',*,*,#26973,.F.) ;
#37367=ORIENTED_EDGE('',*,*,#26974,.T.) ;
#37368=ORIENTED_EDGE('',*,*,#26975,.T.) ;
#37369=ORIENTED_EDGE('',*,*,#26976,.T.) ;
#37370=ORIENTED_EDGE('',*,*,#26977,.T.) ;
#37371=ORIENTED_EDGE('',*,*,#26975,.F.) ;
#37372=ORIENTED_EDGE('',*,*,#26978,.T.) ;
#37373=ORIENTED_EDGE('',*,*,#26972,.T.) ;
#37374=ORIENTED_EDGE('',*,*,#26979,.T.) ;
#37375=ORIENTED_EDGE('',*,*,#26980,.F.) ;
#37376=ORIENTED_EDGE('',*,*,#26981,.F.) ;
#37377=ORIENTED_EDGE('',*,*,#26982,.F.) ;
#37378=ORIENTED_EDGE('',*,*,#26983,.T.) ;
#37379=ORIENTED_EDGE('',*,*,#26984,.T.) ;
#37380=ORIENTED_EDGE('',*,*,#26985,.T.) ;
#37381=ORIENTED_EDGE('',*,*,#26986,.T.) ;
#37382=ORIENTED_EDGE('',*,*,#26987,.T.) ;
#37383=ORIENTED_EDGE('',*,*,#26983,.F.) ;
#37384=ORIENTED_EDGE('',*,*,#26988,.T.) ;
#37385=ORIENTED_EDGE('',*,*,#26981,.T.) ;
#37386=ORIENTED_EDGE('',*,*,#26989,.T.) ;
#37387=ORIENTED_EDGE('',*,*,#26960,.T.) ;
#37388=ORIENTED_EDGE('',*,*,#26990,.T.) ;
#37389=ORIENTED_EDGE('',*,*,#26982,.T.) ;
#37390=ORIENTED_EDGE('',*,*,#26991,.T.) ;
#37391=ORIENTED_EDGE('',*,*,#26992,.F.) ;
#37392=ORIENTED_EDGE('',*,*,#26993,.F.) ;
#37393=ORIENTED_EDGE('',*,*,#26994,.F.) ;
#37394=ORIENTED_EDGE('',*,*,#26995,.T.) ;
#37395=ORIENTED_EDGE('',*,*,#26996,.T.) ;
#37396=ORIENTED_EDGE('',*,*,#26997,.T.) ;
#37397=ORIENTED_EDGE('',*,*,#26998,.T.) ;
#37398=ORIENTED_EDGE('',*,*,#26996,.F.) ;
#37399=ORIENTED_EDGE('',*,*,#26999,.T.) ;
#37400=ORIENTED_EDGE('',*,*,#26993,.T.) ;
#37401=ORIENTED_EDGE('',*,*,#27000,.T.) ;
#37402=ORIENTED_EDGE('',*,*,#27001,.F.) ;
#37403=ORIENTED_EDGE('',*,*,#27002,.F.) ;
#37404=ORIENTED_EDGE('',*,*,#27003,.F.) ;
#37405=ORIENTED_EDGE('',*,*,#27004,.T.) ;
#37406=ORIENTED_EDGE('',*,*,#27005,.T.) ;
#37407=ORIENTED_EDGE('',*,*,#27006,.T.) ;
#37408=ORIENTED_EDGE('',*,*,#27007,.T.) ;
#37409=ORIENTED_EDGE('',*,*,#27005,.F.) ;
#37410=ORIENTED_EDGE('',*,*,#27008,.T.) ;
#37411=ORIENTED_EDGE('',*,*,#27002,.T.) ;
#37412=ORIENTED_EDGE('',*,*,#27009,.T.) ;
#37413=ORIENTED_EDGE('',*,*,#26980,.T.) ;
#37414=ORIENTED_EDGE('',*,*,#27010,.T.) ;
#37415=ORIENTED_EDGE('',*,*,#27003,.T.) ;
#37416=ORIENTED_EDGE('',*,*,#27011,.T.) ;
#37417=ORIENTED_EDGE('',*,*,#27012,.F.) ;
#37418=ORIENTED_EDGE('',*,*,#27013,.F.) ;
#37419=ORIENTED_EDGE('',*,*,#27014,.F.) ;
#37420=ORIENTED_EDGE('',*,*,#27015,.T.) ;
#37421=ORIENTED_EDGE('',*,*,#27016,.T.) ;
#37422=ORIENTED_EDGE('',*,*,#27017,.T.) ;
#37423=ORIENTED_EDGE('',*,*,#27018,.T.) ;
#37424=ORIENTED_EDGE('',*,*,#27019,.T.) ;
#37425=ORIENTED_EDGE('',*,*,#27015,.F.) ;
#37426=ORIENTED_EDGE('',*,*,#27020,.T.) ;
#37427=ORIENTED_EDGE('',*,*,#27013,.T.) ;
#37428=ORIENTED_EDGE('',*,*,#27021,.T.) ;
#37429=ORIENTED_EDGE('',*,*,#27022,.F.) ;
#37430=ORIENTED_EDGE('',*,*,#27023,.F.) ;
#37431=ORIENTED_EDGE('',*,*,#27024,.F.) ;
#37432=ORIENTED_EDGE('',*,*,#27025,.T.) ;
#37433=ORIENTED_EDGE('',*,*,#27026,.T.) ;
#37434=ORIENTED_EDGE('',*,*,#27027,.T.) ;
#37435=ORIENTED_EDGE('',*,*,#27028,.T.) ;
#37436=ORIENTED_EDGE('',*,*,#27026,.F.) ;
#37437=ORIENTED_EDGE('',*,*,#27029,.T.) ;
#37438=ORIENTED_EDGE('',*,*,#27023,.T.) ;
#37439=ORIENTED_EDGE('',*,*,#27030,.T.) ;
#37440=ORIENTED_EDGE('',*,*,#27001,.T.) ;
#37441=ORIENTED_EDGE('',*,*,#27031,.T.) ;
#37442=ORIENTED_EDGE('',*,*,#27024,.T.) ;
#37443=ORIENTED_EDGE('',*,*,#27032,.T.) ;
#37444=ORIENTED_EDGE('',*,*,#27033,.F.) ;
#37445=ORIENTED_EDGE('',*,*,#27034,.F.) ;
#37446=ORIENTED_EDGE('',*,*,#27035,.F.) ;
#37447=ORIENTED_EDGE('',*,*,#27036,.T.) ;
#37448=ORIENTED_EDGE('',*,*,#27037,.T.) ;
#37449=ORIENTED_EDGE('',*,*,#27038,.T.) ;
#37450=ORIENTED_EDGE('',*,*,#27039,.T.) ;
#37451=ORIENTED_EDGE('',*,*,#27037,.F.) ;
#37452=ORIENTED_EDGE('',*,*,#27040,.T.) ;
#37453=ORIENTED_EDGE('',*,*,#27034,.T.) ;
#37454=ORIENTED_EDGE('',*,*,#27041,.T.) ;
#37455=ORIENTED_EDGE('',*,*,#27042,.F.) ;
#37456=ORIENTED_EDGE('',*,*,#27043,.F.) ;
#37457=ORIENTED_EDGE('',*,*,#27044,.F.) ;
#37458=ORIENTED_EDGE('',*,*,#27045,.T.) ;
#37459=ORIENTED_EDGE('',*,*,#27046,.T.) ;
#37460=ORIENTED_EDGE('',*,*,#27047,.T.) ;
#37461=ORIENTED_EDGE('',*,*,#27048,.T.) ;
#37462=ORIENTED_EDGE('',*,*,#27049,.T.) ;
#37463=ORIENTED_EDGE('',*,*,#27045,.F.) ;
#37464=ORIENTED_EDGE('',*,*,#27050,.T.) ;
#37465=ORIENTED_EDGE('',*,*,#27043,.T.) ;
#37466=ORIENTED_EDGE('',*,*,#27051,.T.) ;
#37467=ORIENTED_EDGE('',*,*,#27022,.T.) ;
#37468=ORIENTED_EDGE('',*,*,#27052,.T.) ;
#37469=ORIENTED_EDGE('',*,*,#27044,.T.) ;
#37470=ORIENTED_EDGE('',*,*,#27053,.T.) ;
#37471=ORIENTED_EDGE('',*,*,#27054,.F.) ;
#37472=ORIENTED_EDGE('',*,*,#27055,.F.) ;
#37473=ORIENTED_EDGE('',*,*,#27056,.F.) ;
#37474=ORIENTED_EDGE('',*,*,#27057,.T.) ;
#37475=ORIENTED_EDGE('',*,*,#27058,.T.) ;
#37476=ORIENTED_EDGE('',*,*,#27059,.T.) ;
#37477=ORIENTED_EDGE('',*,*,#27060,.T.) ;
#37478=ORIENTED_EDGE('',*,*,#27058,.F.) ;
#37479=ORIENTED_EDGE('',*,*,#27061,.T.) ;
#37480=ORIENTED_EDGE('',*,*,#27055,.T.) ;
#37481=ORIENTED_EDGE('',*,*,#27062,.T.) ;
#37482=ORIENTED_EDGE('',*,*,#27042,.T.) ;
#37483=ORIENTED_EDGE('',*,*,#27063,.T.) ;
#37484=ORIENTED_EDGE('',*,*,#27056,.T.) ;
#37485=ORIENTED_EDGE('',*,*,#27064,.T.) ;
#37486=ORIENTED_EDGE('',*,*,#27054,.T.) ;
#37487=ORIENTED_EDGE('',*,*,#27065,.T.) ;
#37488=ORIENTED_EDGE('',*,*,#27035,.T.) ;
#37489=ORIENTED_EDGE('',*,*,#27066,.T.) ;
#37490=ORIENTED_EDGE('',*,*,#27033,.T.) ;
#37491=ORIENTED_EDGE('',*,*,#27067,.T.) ;
#37492=ORIENTED_EDGE('',*,*,#27014,.T.) ;
#37493=ORIENTED_EDGE('',*,*,#27068,.T.) ;
#37494=ORIENTED_EDGE('',*,*,#27012,.T.) ;
#37495=ORIENTED_EDGE('',*,*,#27069,.T.) ;
#37496=ORIENTED_EDGE('',*,*,#26994,.T.) ;
#37497=ORIENTED_EDGE('',*,*,#27070,.T.) ;
#37498=ORIENTED_EDGE('',*,*,#26992,.T.) ;
#37499=ORIENTED_EDGE('',*,*,#27071,.T.) ;
#37500=ORIENTED_EDGE('',*,*,#26973,.T.) ;
#37501=ORIENTED_EDGE('',*,*,#27072,.T.) ;
#37502=ORIENTED_EDGE('',*,*,#26971,.T.) ;
#37503=ORIENTED_EDGE('',*,*,#27073,.T.) ;
#37504=ORIENTED_EDGE('',*,*,#26952,.T.) ;
#37505=ORIENTED_EDGE('',*,*,#27074,.T.) ;
#37506=ORIENTED_EDGE('',*,*,#26950,.T.) ;
#37507=ORIENTED_EDGE('',*,*,#27075,.T.) ;
#37508=ORIENTED_EDGE('',*,*,#26943,.T.) ;
#37509=ORIENTED_EDGE('',*,*,#27076,.T.) ;
#37510=ORIENTED_EDGE('',*,*,#26949,.F.) ;
#37511=ORIENTED_EDGE('',*,*,#26970,.F.) ;
#37512=ORIENTED_EDGE('',*,*,#26967,.F.) ;
#37513=ORIENTED_EDGE('',*,*,#27077,.F.) ;
#37514=ORIENTED_EDGE('',*,*,#26968,.F.) ;
#37515=ORIENTED_EDGE('',*,*,#26991,.F.) ;
#37516=ORIENTED_EDGE('',*,*,#26988,.F.) ;
#37517=ORIENTED_EDGE('',*,*,#27078,.F.) ;
#37518=ORIENTED_EDGE('',*,*,#26965,.F.) ;
#37519=ORIENTED_EDGE('',*,*,#27078,.T.) ;
#37520=ORIENTED_EDGE('',*,*,#26987,.F.) ;
#37521=ORIENTED_EDGE('',*,*,#26986,.F.) ;
#37522=ORIENTED_EDGE('',*,*,#27079,.T.) ;
#37523=ORIENTED_EDGE('',*,*,#26989,.F.) ;
#37524=ORIENTED_EDGE('',*,*,#27011,.F.) ;
#37525=ORIENTED_EDGE('',*,*,#27008,.F.) ;
#37526=ORIENTED_EDGE('',*,*,#27080,.F.) ;
#37527=ORIENTED_EDGE('',*,*,#26984,.F.) ;
#37528=ORIENTED_EDGE('',*,*,#27080,.T.) ;
#37529=ORIENTED_EDGE('',*,*,#27007,.F.) ;
#37530=ORIENTED_EDGE('',*,*,#27081,.T.) ;
#37531=ORIENTED_EDGE('',*,*,#26985,.F.) ;
#37532=ORIENTED_EDGE('',*,*,#27009,.F.) ;
#37533=ORIENTED_EDGE('',*,*,#27032,.F.) ;
#37534=ORIENTED_EDGE('',*,*,#27029,.F.) ;
#37535=ORIENTED_EDGE('',*,*,#27082,.F.) ;
#37536=ORIENTED_EDGE('',*,*,#27006,.F.) ;
#37537=ORIENTED_EDGE('',*,*,#27082,.T.) ;
#37538=ORIENTED_EDGE('',*,*,#27028,.F.) ;
#37539=ORIENTED_EDGE('',*,*,#27083,.T.) ;
#37540=ORIENTED_EDGE('',*,*,#27030,.F.) ;
#37541=ORIENTED_EDGE('',*,*,#27053,.F.) ;
#37542=ORIENTED_EDGE('',*,*,#27050,.F.) ;
#37543=ORIENTED_EDGE('',*,*,#27084,.F.) ;
#37544=ORIENTED_EDGE('',*,*,#27027,.F.) ;
#37545=ORIENTED_EDGE('',*,*,#27084,.T.) ;
#37546=ORIENTED_EDGE('',*,*,#27049,.F.) ;
#37547=ORIENTED_EDGE('',*,*,#27048,.F.) ;
#37548=ORIENTED_EDGE('',*,*,#27085,.T.) ;
#37549=ORIENTED_EDGE('',*,*,#27051,.F.) ;
#37550=ORIENTED_EDGE('',*,*,#27064,.F.) ;
#37551=ORIENTED_EDGE('',*,*,#27061,.F.) ;
#37552=ORIENTED_EDGE('',*,*,#27086,.F.) ;
#37553=ORIENTED_EDGE('',*,*,#27046,.F.) ;
#37554=ORIENTED_EDGE('',*,*,#27086,.T.) ;
#37555=ORIENTED_EDGE('',*,*,#27060,.F.) ;
#37556=ORIENTED_EDGE('',*,*,#27087,.T.) ;
#37557=ORIENTED_EDGE('',*,*,#27047,.F.) ;
#37558=ORIENTED_EDGE('',*,*,#27088,.F.) ;
#37559=ORIENTED_EDGE('',*,*,#27057,.F.) ;
#37560=ORIENTED_EDGE('',*,*,#27063,.F.) ;
#37561=ORIENTED_EDGE('',*,*,#27052,.F.) ;
#37562=ORIENTED_EDGE('',*,*,#27025,.F.) ;
#37563=ORIENTED_EDGE('',*,*,#27031,.F.) ;
#37564=ORIENTED_EDGE('',*,*,#27004,.F.) ;
#37565=ORIENTED_EDGE('',*,*,#27010,.F.) ;
#37566=ORIENTED_EDGE('',*,*,#26990,.F.) ;
#37567=ORIENTED_EDGE('',*,*,#26963,.F.) ;
#37568=ORIENTED_EDGE('',*,*,#26969,.F.) ;
#37569=ORIENTED_EDGE('',*,*,#26944,.F.) ;
#37570=ORIENTED_EDGE('',*,*,#27075,.F.) ;
#37571=ORIENTED_EDGE('',*,*,#27073,.F.) ;
#37572=ORIENTED_EDGE('',*,*,#26974,.F.) ;
#37573=ORIENTED_EDGE('',*,*,#27071,.F.) ;
#37574=ORIENTED_EDGE('',*,*,#26995,.F.) ;
#37575=ORIENTED_EDGE('',*,*,#27069,.F.) ;
#37576=ORIENTED_EDGE('',*,*,#27067,.F.) ;
#37577=ORIENTED_EDGE('',*,*,#27036,.F.) ;
#37578=ORIENTED_EDGE('',*,*,#27065,.F.) ;
#37579=ORIENTED_EDGE('',*,*,#27018,.F.) ;
#37580=ORIENTED_EDGE('',*,*,#27089,.T.) ;
#37581=ORIENTED_EDGE('',*,*,#27038,.F.) ;
#37582=ORIENTED_EDGE('',*,*,#27090,.T.) ;
#37583=ORIENTED_EDGE('',*,*,#27019,.F.) ;
#37584=ORIENTED_EDGE('',*,*,#27039,.F.) ;
#37585=ORIENTED_EDGE('',*,*,#27091,.T.) ;
#37586=ORIENTED_EDGE('',*,*,#27059,.F.) ;
#37587=ORIENTED_EDGE('',*,*,#27092,.T.) ;
#37588=ORIENTED_EDGE('',*,*,#26946,.F.) ;
#37589=ORIENTED_EDGE('',*,*,#27077,.T.) ;
#37590=ORIENTED_EDGE('',*,*,#26966,.F.) ;
#37591=ORIENTED_EDGE('',*,*,#27093,.T.) ;
#37592=ORIENTED_EDGE('',*,*,#26947,.F.) ;
#37593=ORIENTED_EDGE('',*,*,#27094,.T.) ;
#37594=ORIENTED_EDGE('',*,*,#26955,.F.) ;
#37595=ORIENTED_EDGE('',*,*,#26954,.F.) ;
#37596=ORIENTED_EDGE('',*,*,#27095,.T.) ;
#37597=ORIENTED_EDGE('',*,*,#26956,.F.) ;
#37598=ORIENTED_EDGE('',*,*,#27096,.T.) ;
#37599=ORIENTED_EDGE('',*,*,#26976,.F.) ;
#37600=ORIENTED_EDGE('',*,*,#27097,.T.) ;
#37601=ORIENTED_EDGE('',*,*,#26957,.F.) ;
#37602=ORIENTED_EDGE('',*,*,#26977,.F.) ;
#37603=ORIENTED_EDGE('',*,*,#27098,.T.) ;
#37604=ORIENTED_EDGE('',*,*,#26997,.F.) ;
#37605=ORIENTED_EDGE('',*,*,#27099,.T.) ;
#37606=ORIENTED_EDGE('',*,*,#26998,.F.) ;
#37607=ORIENTED_EDGE('',*,*,#27100,.T.) ;
#37608=ORIENTED_EDGE('',*,*,#27017,.F.) ;
#37609=ORIENTED_EDGE('',*,*,#27016,.F.) ;
#37610=ORIENTED_EDGE('',*,*,#27101,.T.) ;
#37611=ORIENTED_EDGE('',*,*,#26948,.F.) ;
#37612=ORIENTED_EDGE('',*,*,#27095,.F.) ;
#37613=ORIENTED_EDGE('',*,*,#26959,.F.) ;
#37614=ORIENTED_EDGE('',*,*,#27076,.F.) ;
#37615=ORIENTED_EDGE('',*,*,#26958,.F.) ;
#37616=ORIENTED_EDGE('',*,*,#27097,.F.) ;
#37617=ORIENTED_EDGE('',*,*,#26979,.F.) ;
#37618=ORIENTED_EDGE('',*,*,#27074,.F.) ;
#37619=ORIENTED_EDGE('',*,*,#26978,.F.) ;
#37620=ORIENTED_EDGE('',*,*,#27099,.F.) ;
#37621=ORIENTED_EDGE('',*,*,#27000,.F.) ;
#37622=ORIENTED_EDGE('',*,*,#27072,.F.) ;
#37623=ORIENTED_EDGE('',*,*,#26999,.F.) ;
#37624=ORIENTED_EDGE('',*,*,#27101,.F.) ;
#37625=ORIENTED_EDGE('',*,*,#27021,.F.) ;
#37626=ORIENTED_EDGE('',*,*,#27070,.F.) ;
#37627=ORIENTED_EDGE('',*,*,#27020,.F.) ;
#37628=ORIENTED_EDGE('',*,*,#27090,.F.) ;
#37629=ORIENTED_EDGE('',*,*,#27041,.F.) ;
#37630=ORIENTED_EDGE('',*,*,#27068,.F.) ;
#37631=ORIENTED_EDGE('',*,*,#27089,.F.) ;
#37632=ORIENTED_EDGE('',*,*,#27100,.F.) ;
#37633=ORIENTED_EDGE('',*,*,#27098,.F.) ;
#37634=ORIENTED_EDGE('',*,*,#27096,.F.) ;
#37635=ORIENTED_EDGE('',*,*,#27094,.F.) ;
#37636=ORIENTED_EDGE('',*,*,#27093,.F.) ;
#37637=ORIENTED_EDGE('',*,*,#27079,.F.) ;
#37638=ORIENTED_EDGE('',*,*,#27081,.F.) ;
#37639=ORIENTED_EDGE('',*,*,#27083,.F.) ;
#37640=ORIENTED_EDGE('',*,*,#27085,.F.) ;
#37641=ORIENTED_EDGE('',*,*,#27087,.F.) ;
#37642=ORIENTED_EDGE('',*,*,#27091,.F.) ;
#37643=ORIENTED_EDGE('',*,*,#27088,.T.) ;
#37644=ORIENTED_EDGE('',*,*,#27102,.T.) ;
#37645=ORIENTED_EDGE('',*,*,#27103,.T.) ;
#37646=ORIENTED_EDGE('',*,*,#27102,.F.) ;
#37647=ORIENTED_EDGE('',*,*,#27103,.F.) ;
#37648=ORIENTED_EDGE('',*,*,#27104,.T.) ;
#37649=ORIENTED_EDGE('',*,*,#27105,.F.) ;
#37650=ORIENTED_EDGE('',*,*,#27106,.F.) ;
#37651=ORIENTED_EDGE('',*,*,#27104,.F.) ;
#37652=ORIENTED_EDGE('',*,*,#27107,.T.) ;
#37653=ORIENTED_EDGE('',*,*,#27108,.T.) ;
#37654=ORIENTED_EDGE('',*,*,#27105,.T.) ;
#37655=ORIENTED_EDGE('',*,*,#27106,.T.) ;
#37656=ORIENTED_EDGE('',*,*,#27108,.F.) ;
#37657=ORIENTED_EDGE('',*,*,#27107,.F.) ;
#37658=ORIENTED_EDGE('',*,*,#27040,.F.) ;
#37659=ORIENTED_EDGE('',*,*,#27092,.F.) ;
#37660=ORIENTED_EDGE('',*,*,#27062,.F.) ;
#37661=ORIENTED_EDGE('',*,*,#27066,.F.) ;
#45697=TOROIDAL_SURFACE('',#52018,0.240000000000009,0.120000000000005) ;
#45698=TOROIDAL_SURFACE('',#52037,0.240000000000009,0.120000000000005) ;
#45699=TOROIDAL_SURFACE('',#52047,0.240000000000009,0.120000000000005) ;
#45700=TOROIDAL_SURFACE('',#52067,0.240000000000009,0.120000000000005) ;
#45701=TOROIDAL_SURFACE('',#52076,0.240000000000009,0.120000000000005) ;
#45702=TOROIDAL_SURFACE('',#52096,0.240000000000009,0.120000000000005) ;
#45703=TOROIDAL_SURFACE('',#52106,0.240000000000009,0.120000000000005) ;
#45704=TOROIDAL_SURFACE('',#52126,0.24,0.119999999999996) ;
#45705=TOROIDAL_SURFACE('',#52168,1.74999999999999,0.25) ;
#45706=TOROIDAL_SURFACE('',#52174,1.74999999999999,0.25) ;
#47334=ADVANCED_FACE('',(#12116),#45697,.T.) ;
#47335=ADVANCED_FACE('',(#12117),#1991,.T.) ;
#47336=ADVANCED_FACE('',(#12118),#9993,.F.) ;
#47337=ADVANCED_FACE('',(#12119),#2195,.T.) ;
#47338=ADVANCED_FACE('',(#12120),#1992,.F.) ;
#47339=ADVANCED_FACE('',(#12121),#9994,.T.) ;
#47340=ADVANCED_FACE('',(#12122),#45698,.T.) ;
#47341=ADVANCED_FACE('',(#12123),#1993,.T.) ;
#47342=ADVANCED_FACE('',(#12124),#9995,.F.) ;
#47343=ADVANCED_FACE('',(#12125),#9996,.T.) ;
#47344=ADVANCED_FACE('',(#12126),#45699,.T.) ;
#47345=ADVANCED_FACE('',(#12127),#1994,.T.) ;
#47346=ADVANCED_FACE('',(#12128),#9997,.F.) ;
#47347=ADVANCED_FACE('',(#12129),#2196,.T.) ;
#47348=ADVANCED_FACE('',(#12130),#1995,.F.) ;
#47349=ADVANCED_FACE('',(#12131),#9998,.T.) ;
#47350=ADVANCED_FACE('',(#12132),#9999,.T.) ;
#47351=ADVANCED_FACE('',(#12133),#45700,.T.) ;
#47352=ADVANCED_FACE('',(#12134),#1996,.T.) ;
#47353=ADVANCED_FACE('',(#12135),#10000,.F.) ;
#47354=ADVANCED_FACE('',(#12136),#45701,.T.) ;
#47355=ADVANCED_FACE('',(#12137),#1997,.T.) ;
#47356=ADVANCED_FACE('',(#12138),#10001,.F.) ;
#47357=ADVANCED_FACE('',(#12139),#10002,.T.) ;
#47358=ADVANCED_FACE('',(#12140),#2197,.T.) ;
#47359=ADVANCED_FACE('',(#12141),#1998,.F.) ;
#47360=ADVANCED_FACE('',(#12142),#10003,.T.) ;
#47361=ADVANCED_FACE('',(#12143),#45702,.T.) ;
#47362=ADVANCED_FACE('',(#12144),#1999,.T.) ;
#47363=ADVANCED_FACE('',(#12145),#10004,.F.) ;
#47364=ADVANCED_FACE('',(#12146),#10005,.T.) ;
#47365=ADVANCED_FACE('',(#12147),#45703,.T.) ;
#47366=ADVANCED_FACE('',(#12148),#2000,.T.) ;
#47367=ADVANCED_FACE('',(#12149),#10006,.F.) ;
#47368=ADVANCED_FACE('',(#12150),#2198,.T.) ;
#47369=ADVANCED_FACE('',(#12151),#2001,.F.) ;
#47370=ADVANCED_FACE('',(#12152),#10007,.T.) ;
#47371=ADVANCED_FACE('',(#12153),#10008,.T.) ;
#47372=ADVANCED_FACE('',(#12154),#45704,.T.) ;
#47373=ADVANCED_FACE('',(#12155),#2002,.T.) ;
#47374=ADVANCED_FACE('',(#12156),#10009,.F.) ;
#47375=ADVANCED_FACE('',(#12157),#10010,.T.) ;
#47376=ADVANCED_FACE('',(#12158),#10011,.T.) ;
#47377=ADVANCED_FACE('',(#12159),#10012,.T.) ;
#47378=ADVANCED_FACE('',(#12160),#10013,.T.) ;
#47379=ADVANCED_FACE('',(#12161),#10014,.T.) ;
#47380=ADVANCED_FACE('',(#12162),#10015,.T.) ;
#47381=ADVANCED_FACE('',(#12163),#10016,.T.) ;
#47382=ADVANCED_FACE('',(#12164),#2486,.T.) ;
#47383=ADVANCED_FACE('',(#12165),#2487,.T.) ;
#47384=ADVANCED_FACE('',(#12166),#10017,.F.) ;
#47385=ADVANCED_FACE('',(#12167),#2488,.T.) ;
#47386=ADVANCED_FACE('',(#12168),#10018,.F.) ;
#47387=ADVANCED_FACE('',(#12169),#2489,.T.) ;
#47388=ADVANCED_FACE('',(#12170),#10019,.F.) ;
#47389=ADVANCED_FACE('',(#12171),#2490,.T.) ;
#47390=ADVANCED_FACE('',(#12172),#10020,.F.) ;
#47391=ADVANCED_FACE('',(#12173),#2491,.T.) ;
#47392=ADVANCED_FACE('',(#12174),#10021,.F.) ;
#47393=ADVANCED_FACE('',(#12175,#733),#2492,.F.) ;
#47394=ADVANCED_FACE('',(#12176),#10022,.F.) ;
#47395=ADVANCED_FACE('',(#12177),#10023,.F.) ;
#47396=ADVANCED_FACE('',(#12178),#10024,.F.) ;
#47397=ADVANCED_FACE('',(#12179),#10025,.F.) ;
#47398=ADVANCED_FACE('',(#12180),#10026,.F.) ;
#47399=ADVANCED_FACE('',(#12181),#10027,.F.) ;
#47400=ADVANCED_FACE('',(#12182),#10028,.F.) ;
#47401=ADVANCED_FACE('',(#12183),#2493,.T.) ;
#47402=ADVANCED_FACE('',(#12184),#2494,.T.) ;
#47403=ADVANCED_FACE('',(#12185),#2495,.T.) ;
#47404=ADVANCED_FACE('',(#12186),#2496,.T.) ;
#47405=ADVANCED_FACE('',(#12187),#2497,.T.) ;
#47406=ADVANCED_FACE('',(#12188),#2498,.T.) ;
#47407=ADVANCED_FACE('',(#12189),#45705,.T.) ;
#47408=ADVANCED_FACE('',(#12190),#10029,.T.) ;
#47409=ADVANCED_FACE('',(#12191),#45706,.T.) ;
#47410=ADVANCED_FACE('',(#12192),#2499,.T.) ;
#47411=ADVANCED_FACE('',(#12193),#2500,.T.) ;
#49066=CLOSED_SHELL('',(#47334,#47335,#47336,#47337,#47338,#47339,#47340,
#47341,#47342,#47343,#47344,#47345,#47346,#47347,#47348,#47349,#47350,#47351,
#47352,#47353,#47354,#47355,#47356,#47357,#47358,#47359,#47360,#47361,#47362,
#47363,#47364,#47365,#47366,#47367,#47368,#47369,#47370,#47371,#47372,#47373,
#47374,#47375,#47376,#47377,#47378,#47379,#47380,#47381,#47382,#47383,#47384,
#47385,#47386,#47387,#47388,#47389,#47390,#47391,#47392,#47393,#47394,#47395,
#47396,#47397,#47398,#47399,#47400,#47401,#47402,#47403,#47404,#47405,#47406,
#47407,#47408,#47409,#47410,#47411)) ;
#52017=AXIS2_PLACEMENT_3D('',#87531,#61750,#61751) ;
#52018=AXIS2_PLACEMENT_3D('',#87532,#61752,#61753) ;
#52019=AXIS2_PLACEMENT_3D('',#87535,#61754,#61755) ;
#52020=AXIS2_PLACEMENT_3D('',#87537,#61756,#61757) ;
#52021=AXIS2_PLACEMENT_3D('',#87539,#61758,#61759) ;
#52022=AXIS2_PLACEMENT_3D('',#87540,#61760,#61761) ;
#52023=AXIS2_PLACEMENT_3D('',#87563,#61762,#61763) ;
#52024=AXIS2_PLACEMENT_3D('',#87565,#61764,#61765) ;
#52025=AXIS2_PLACEMENT_3D('',#87566,#61766,#61767) ;
#52026=AXIS2_PLACEMENT_3D('',#87567,#61768,#61769) ;
#52027=AXIS2_PLACEMENT_3D('',#87570,#61772,#61773) ;
#52028=AXIS2_PLACEMENT_3D('',#87573,#61774,#61775) ;
#52029=AXIS2_PLACEMENT_3D('',#87575,#61776,#61777) ;
#52030=AXIS2_PLACEMENT_3D('',#87576,#61778,#61779) ;
#52031=AXIS2_PLACEMENT_3D('',#87604,#61780,#61781) ;
#52032=AXIS2_PLACEMENT_3D('',#87606,#61782,#61783) ;
#52033=AXIS2_PLACEMENT_3D('',#87608,#61784,#61785) ;
#52034=AXIS2_PLACEMENT_3D('',#87610,#61786,#61787) ;
#52035=AXIS2_PLACEMENT_3D('',#87611,#61788,#61789) ;
#52036=AXIS2_PLACEMENT_3D('',#87612,#61790,#61791) ;
#52037=AXIS2_PLACEMENT_3D('',#87615,#61794,#61795) ;
#52038=AXIS2_PLACEMENT_3D('',#87618,#61796,#61797) ;
#52039=AXIS2_PLACEMENT_3D('',#87620,#61798,#61799) ;
#52040=AXIS2_PLACEMENT_3D('',#87622,#61800,#61801) ;
#52041=AXIS2_PLACEMENT_3D('',#87623,#61802,#61803) ;
#52042=AXIS2_PLACEMENT_3D('',#87646,#61804,#61805) ;
#52043=AXIS2_PLACEMENT_3D('',#87648,#61806,#61807) ;
#52044=AXIS2_PLACEMENT_3D('',#87649,#61808,#61809) ;
#52045=AXIS2_PLACEMENT_3D('',#87650,#61810,#61811) ;
#52046=AXIS2_PLACEMENT_3D('',#87653,#61814,#61815) ;
#52047=AXIS2_PLACEMENT_3D('',#87656,#61818,#61819) ;
#52048=AXIS2_PLACEMENT_3D('',#87659,#61820,#61821) ;
#52049=AXIS2_PLACEMENT_3D('',#87661,#61822,#61823) ;
#52050=AXIS2_PLACEMENT_3D('',#87663,#61824,#61825) ;
#52051=AXIS2_PLACEMENT_3D('',#87664,#61826,#61827) ;
#52052=AXIS2_PLACEMENT_3D('',#87687,#61828,#61829) ;
#52053=AXIS2_PLACEMENT_3D('',#87689,#61830,#61831) ;
#52054=AXIS2_PLACEMENT_3D('',#87690,#61832,#61833) ;
#52055=AXIS2_PLACEMENT_3D('',#87691,#61834,#61835) ;
#52056=AXIS2_PLACEMENT_3D('',#87694,#61838,#61839) ;
#52057=AXIS2_PLACEMENT_3D('',#87697,#61840,#61841) ;
#52058=AXIS2_PLACEMENT_3D('',#87699,#61842,#61843) ;
#52059=AXIS2_PLACEMENT_3D('',#87700,#61844,#61845) ;
#52060=AXIS2_PLACEMENT_3D('',#87728,#61846,#61847) ;
#52061=AXIS2_PLACEMENT_3D('',#87730,#61848,#61849) ;
#52062=AXIS2_PLACEMENT_3D('',#87732,#61850,#61851) ;
#52063=AXIS2_PLACEMENT_3D('',#87734,#61852,#61853) ;
#52064=AXIS2_PLACEMENT_3D('',#87735,#61854,#61855) ;
#52065=AXIS2_PLACEMENT_3D('',#87736,#61856,#61857) ;
#52066=AXIS2_PLACEMENT_3D('',#87739,#61860,#61861) ;
#52067=AXIS2_PLACEMENT_3D('',#87742,#61864,#61865) ;
#52068=AXIS2_PLACEMENT_3D('',#87745,#61866,#61867) ;
#52069=AXIS2_PLACEMENT_3D('',#87747,#61868,#61869) ;
#52070=AXIS2_PLACEMENT_3D('',#87749,#61870,#61871) ;
#52071=AXIS2_PLACEMENT_3D('',#87750,#61872,#61873) ;
#52072=AXIS2_PLACEMENT_3D('',#87773,#61874,#61875) ;
#52073=AXIS2_PLACEMENT_3D('',#87775,#61876,#61877) ;
#52074=AXIS2_PLACEMENT_3D('',#87776,#61878,#61879) ;
#52075=AXIS2_PLACEMENT_3D('',#87777,#61880,#61881) ;
#52076=AXIS2_PLACEMENT_3D('',#87780,#61884,#61885) ;
#52077=AXIS2_PLACEMENT_3D('',#87783,#61886,#61887) ;
#52078=AXIS2_PLACEMENT_3D('',#87785,#61888,#61889) ;
#52079=AXIS2_PLACEMENT_3D('',#87787,#61890,#61891) ;
#52080=AXIS2_PLACEMENT_3D('',#87788,#61892,#61893) ;
#52081=AXIS2_PLACEMENT_3D('',#87811,#61894,#61895) ;
#52082=AXIS2_PLACEMENT_3D('',#87813,#61896,#61897) ;
#52083=AXIS2_PLACEMENT_3D('',#87814,#61898,#61899) ;
#52084=AXIS2_PLACEMENT_3D('',#87815,#61900,#61901) ;
#52085=AXIS2_PLACEMENT_3D('',#87818,#61904,#61905) ;
#52086=AXIS2_PLACEMENT_3D('',#87821,#61908,#61909) ;
#52087=AXIS2_PLACEMENT_3D('',#87824,#61910,#61911) ;
#52088=AXIS2_PLACEMENT_3D('',#87826,#61912,#61913) ;
#52089=AXIS2_PLACEMENT_3D('',#87827,#61914,#61915) ;
#52090=AXIS2_PLACEMENT_3D('',#87855,#61916,#61917) ;
#52091=AXIS2_PLACEMENT_3D('',#87857,#61918,#61919) ;
#52092=AXIS2_PLACEMENT_3D('',#87859,#61920,#61921) ;
#52093=AXIS2_PLACEMENT_3D('',#87861,#61922,#61923) ;
#52094=AXIS2_PLACEMENT_3D('',#87862,#61924,#61925) ;
#52095=AXIS2_PLACEMENT_3D('',#87863,#61926,#61927) ;
#52096=AXIS2_PLACEMENT_3D('',#87866,#61930,#61931) ;
#52097=AXIS2_PLACEMENT_3D('',#87869,#61932,#61933) ;
#52098=AXIS2_PLACEMENT_3D('',#87871,#61934,#61935) ;
#52099=AXIS2_PLACEMENT_3D('',#87873,#61936,#61937) ;
#52100=AXIS2_PLACEMENT_3D('',#87874,#61938,#61939) ;
#52101=AXIS2_PLACEMENT_3D('',#87897,#61940,#61941) ;
#52102=AXIS2_PLACEMENT_3D('',#87899,#61942,#61943) ;
#52103=AXIS2_PLACEMENT_3D('',#87900,#61944,#61945) ;
#52104=AXIS2_PLACEMENT_3D('',#87901,#61946,#61947) ;
#52105=AXIS2_PLACEMENT_3D('',#87904,#61950,#61951) ;
#52106=AXIS2_PLACEMENT_3D('',#87907,#61954,#61955) ;
#52107=AXIS2_PLACEMENT_3D('',#87910,#61956,#61957) ;
#52108=AXIS2_PLACEMENT_3D('',#87912,#61958,#61959) ;
#52109=AXIS2_PLACEMENT_3D('',#87914,#61960,#61961) ;
#52110=AXIS2_PLACEMENT_3D('',#87915,#61962,#61963) ;
#52111=AXIS2_PLACEMENT_3D('',#87938,#61964,#61965) ;
#52112=AXIS2_PLACEMENT_3D('',#87940,#61966,#61967) ;
#52113=AXIS2_PLACEMENT_3D('',#87941,#61968,#61969) ;
#52114=AXIS2_PLACEMENT_3D('',#87942,#61970,#61971) ;
#52115=AXIS2_PLACEMENT_3D('',#87945,#61974,#61975) ;
#52116=AXIS2_PLACEMENT_3D('',#87948,#61976,#61977) ;
#52117=AXIS2_PLACEMENT_3D('',#87950,#61978,#61979) ;
#52118=AXIS2_PLACEMENT_3D('',#87951,#61980,#61981) ;
#52119=AXIS2_PLACEMENT_3D('',#87979,#61982,#61983) ;
#52120=AXIS2_PLACEMENT_3D('',#87981,#61984,#61985) ;
#52121=AXIS2_PLACEMENT_3D('',#87983,#61986,#61987) ;
#52122=AXIS2_PLACEMENT_3D('',#87985,#61988,#61989) ;
#52123=AXIS2_PLACEMENT_3D('',#87986,#61990,#61991) ;
#52124=AXIS2_PLACEMENT_3D('',#87987,#61992,#61993) ;
#52125=AXIS2_PLACEMENT_3D('',#87990,#61996,#61997) ;
#52126=AXIS2_PLACEMENT_3D('',#87993,#62000,#62001) ;
#52127=AXIS2_PLACEMENT_3D('',#87996,#62002,#62003) ;
#52128=AXIS2_PLACEMENT_3D('',#87998,#62004,#62005) ;
#52129=AXIS2_PLACEMENT_3D('',#88000,#62006,#62007) ;
#52130=AXIS2_PLACEMENT_3D('',#88001,#62008,#62009) ;
#52131=AXIS2_PLACEMENT_3D('',#88024,#62010,#62011) ;
#52132=AXIS2_PLACEMENT_3D('',#88026,#62012,#62013) ;
#52133=AXIS2_PLACEMENT_3D('',#88027,#62014,#62015) ;
#52134=AXIS2_PLACEMENT_3D('',#88028,#62016,#62017) ;
#52135=AXIS2_PLACEMENT_3D('',#88031,#62020,#62021) ;
#52136=AXIS2_PLACEMENT_3D('',#88034,#62024,#62025) ;
#52137=AXIS2_PLACEMENT_3D('',#88037,#62028,#62029) ;
#52138=AXIS2_PLACEMENT_3D('',#88040,#62032,#62033) ;
#52139=AXIS2_PLACEMENT_3D('',#88043,#62036,#62037) ;
#52140=AXIS2_PLACEMENT_3D('',#88046,#62040,#62041) ;
#52141=AXIS2_PLACEMENT_3D('',#88049,#62044,#62045) ;
#52142=AXIS2_PLACEMENT_3D('',#88052,#62048,#62049) ;
#52143=AXIS2_PLACEMENT_3D('',#88054,#62051,#62052) ;
#52144=AXIS2_PLACEMENT_3D('',#88056,#62054,#62055) ;
#52145=AXIS2_PLACEMENT_3D('',#88058,#62057,#62058) ;
#52146=AXIS2_PLACEMENT_3D('',#88060,#62060,#62061) ;
#52147=AXIS2_PLACEMENT_3D('',#88062,#62063,#62064) ;
#52148=AXIS2_PLACEMENT_3D('',#88064,#62066,#62067) ;
#52149=AXIS2_PLACEMENT_3D('',#88066,#62069,#62070) ;
#52150=AXIS2_PLACEMENT_3D('',#88068,#62072,#62073) ;
#52151=AXIS2_PLACEMENT_3D('',#88070,#62075,#62076) ;
#52152=AXIS2_PLACEMENT_3D('',#88072,#62078,#62079) ;
#52153=AXIS2_PLACEMENT_3D('',#88074,#62081,#62082) ;
#52154=AXIS2_PLACEMENT_3D('',#88076,#62083,#62084) ;
#52155=AXIS2_PLACEMENT_3D('',#88077,#62085,#62086) ;
#52156=AXIS2_PLACEMENT_3D('',#88080,#62089,#62090) ;
#52157=AXIS2_PLACEMENT_3D('',#88083,#62093,#62094) ;
#52158=AXIS2_PLACEMENT_3D('',#88085,#62096,#62097) ;
#52159=AXIS2_PLACEMENT_3D('',#88088,#62100,#62101) ;
#52160=AXIS2_PLACEMENT_3D('',#88091,#62104,#62105) ;
#52161=AXIS2_PLACEMENT_3D('',#88094,#62108,#62109) ;
#52162=AXIS2_PLACEMENT_3D('',#88097,#62112,#62113) ;
#52163=AXIS2_PLACEMENT_3D('',#88098,#62114,#62115) ;
#52164=AXIS2_PLACEMENT_3D('',#88099,#62116,#62117) ;
#52165=AXIS2_PLACEMENT_3D('',#88100,#62118,#62119) ;
#52166=AXIS2_PLACEMENT_3D('',#88101,#62120,#62121) ;
#52167=AXIS2_PLACEMENT_3D('',#88102,#62122,#62123) ;
#52168=AXIS2_PLACEMENT_3D('',#88103,#62124,#62125) ;
#52169=AXIS2_PLACEMENT_3D('',#88105,#62126,#62127) ;
#52170=AXIS2_PLACEMENT_3D('',#88106,#62128,#62129) ;
#52171=AXIS2_PLACEMENT_3D('',#88107,#62130,#62131) ;
#52172=AXIS2_PLACEMENT_3D('',#88111,#62133,#62134) ;
#52173=AXIS2_PLACEMENT_3D('',#88112,#62135,#62136) ;
#52174=AXIS2_PLACEMENT_3D('',#88113,#62137,#62138) ;
#52175=AXIS2_PLACEMENT_3D('',#88115,#62139,#62140) ;
#52176=AXIS2_PLACEMENT_3D('',#88116,#62141,#62142) ;
#52177=AXIS2_PLACEMENT_3D('',#88117,#62143,#62144) ;
#52178=AXIS2_PLACEMENT_3D('',#88118,#62145,#62146) ;
#61750=DIRECTION('axis',(0.,0.,1.)) ;
#61751=DIRECTION('refdir',(1.,0.,0.)) ;
#61752=DIRECTION('center_axis',(0.,0.,-1.)) ;
#61753=DIRECTION('ref_axis',(-1.,0.,0.)) ;
#61754=DIRECTION('center_axis',(0.,1.,0.)) ;
#61755=DIRECTION('ref_axis',(-1.,0.,0.)) ;
#61756=DIRECTION('center_axis',(0.,0.,-1.)) ;
#61757=DIRECTION('ref_axis',(0.,-1.,0.)) ;
#61758=DIRECTION('center_axis',(-1.,0.,0.)) ;
#61759=DIRECTION('ref_axis',(0.,0.,1.)) ;
#61760=DIRECTION('center_axis',(-2.52374105052742E-18,-5.60383084497445E-34,
1.)) ;
#61761=DIRECTION('ref_axis',(0.707106781186548,-0.707106781186548,1.7845544107868E-18)) ;
#61762=DIRECTION('center_axis',(0.,0.,1.)) ;
#61763=DIRECTION('ref_axis',(0.,-1.,0.)) ;
#61764=DIRECTION('center_axis',(0.461352736642031,0.887216801234573,0.)) ;
#61765=DIRECTION('ref_axis',(0.887216801234573,-0.461352736642031,0.)) ;
#61766=DIRECTION('center_axis',(-0.887216801234586,-0.461352736642007,0.)) ;
#61767=DIRECTION('ref_axis',(0.461352736642007,-0.887216801234586,0.)) ;
#61768=DIRECTION('center_axis',(0.,0.,1.)) ;
#61769=DIRECTION('ref_axis',(0.707106781186547,-0.707106781186547,0.)) ;
#61770=DIRECTION('',(0.,0.,1.)) ;
#61771=DIRECTION('',(0.,0.,-1.)) ;
#61772=DIRECTION('center_axis',(-0.816496580927736,-0.408248290463809,-0.408248290463898)) ;
#61773=DIRECTION('ref_axis',(-0.577350269189577,0.577350269189695,0.577350269189606)) ;
#61774=DIRECTION('center_axis',(-1.,0.,0.)) ;
#61775=DIRECTION('ref_axis',(0.,1.,0.)) ;
#61776=DIRECTION('center_axis',(0.,0.,1.)) ;
#61777=DIRECTION('ref_axis',(-1.,0.,0.)) ;
#61778=DIRECTION('center_axis',(0.,1.,0.)) ;
#61779=DIRECTION('ref_axis',(0.,0.,1.)) ;
#61780=DIRECTION('center_axis',(0.,0.,-1.)) ;
#61781=DIRECTION('ref_axis',(-1.,0.,0.)) ;
#61782=DIRECTION('center_axis',(0.559857411277938,0.828588968691453,0.)) ;
#61783=DIRECTION('ref_axis',(0.828588968691453,-0.559857411277938,0.)) ;
#61784=DIRECTION('center_axis',(0.559857411277938,0.828588968691453,0.)) ;
#61785=DIRECTION('ref_axis',(0.828588968691453,-0.559857411277938,0.)) ;
#61786=DIRECTION('center_axis',(-0.82858896869141,-0.559857411278002,0.)) ;
#61787=DIRECTION('ref_axis',(0.559857411278002,-0.82858896869141,0.)) ;
#61788=DIRECTION('center_axis',(-0.82858896869141,-0.559857411278002,0.)) ;
#61789=DIRECTION('ref_axis',(0.559857411278002,-0.82858896869141,0.)) ;
#61790=DIRECTION('center_axis',(0.,0.,1.)) ;
#61791=DIRECTION('ref_axis',(-0.707106781186547,0.707106781186547,0.)) ;
#61792=DIRECTION('',(0.,0.,1.)) ;
#61793=DIRECTION('',(0.,0.,-1.)) ;
#61794=DIRECTION('center_axis',(0.,0.,-1.)) ;
#61795=DIRECTION('ref_axis',(-1.,0.,0.)) ;
#61796=DIRECTION('center_axis',(-1.,0.,0.)) ;
#61797=DIRECTION('ref_axis',(0.,-1.,0.)) ;
#61798=DIRECTION('center_axis',(0.,0.,-1.)) ;
#61799=DIRECTION('ref_axis',(1.,0.,0.)) ;
#61800=DIRECTION('center_axis',(0.,-1.,0.)) ;
#61801=DIRECTION('ref_axis',(0.,0.,1.)) ;
#61802=DIRECTION('center_axis',(-2.52374105052742E-18,-5.60383084497445E-34,
1.)) ;
#61803=DIRECTION('ref_axis',(0.707106781186548,0.707106781186548,1.7845544107868E-18)) ;
#61804=DIRECTION('center_axis',(0.,0.,1.)) ;
#61805=DIRECTION('ref_axis',(1.,0.,0.)) ;
#61806=DIRECTION('center_axis',(-0.88721680123456,0.461352736642057,0.)) ;
#61807=DIRECTION('ref_axis',(0.461352736642057,0.88721680123456,0.)) ;
#61808=DIRECTION('center_axis',(0.461352736642031,-0.887216801234573,0.)) ;
#61809=DIRECTION('ref_axis',(0.887216801234573,0.461352736642031,0.)) ;
#61810=DIRECTION('center_axis',(0.,0.,1.)) ;
#61811=DIRECTION('ref_axis',(0.707106781186547,0.707106781186547,0.)) ;
#61812=DIRECTION('',(0.,0.,1.)) ;
#61813=DIRECTION('',(0.,0.,-1.)) ;
#61814=DIRECTION('center_axis',(1.41426179436738E-51,-1.,-5.60383084497445E-34)) ;
#61815=DIRECTION('ref_axis',(-0.707106781186547,-3.96250679110377E-34,0.707106781186547)) ;
#61816=DIRECTION('',(-1.41426179436738E-51,1.,5.60383084497445E-34)) ;
#61817=DIRECTION('',(1.41426179436738E-51,-1.,-5.60383084497445E-34)) ;
#61818=DIRECTION('center_axis',(0.,0.,-1.)) ;
#61819=DIRECTION('ref_axis',(-1.,0.,0.)) ;
#61820=DIRECTION('center_axis',(0.,1.,0.)) ;
#61821=DIRECTION('ref_axis',(-1.,0.,0.)) ;
#61822=DIRECTION('center_axis',(0.,0.,-1.)) ;
#61823=DIRECTION('ref_axis',(0.,-1.,0.)) ;
#61824=DIRECTION('center_axis',(-1.,0.,0.)) ;
#61825=DIRECTION('ref_axis',(0.,0.,1.)) ;
#61826=DIRECTION('center_axis',(-2.52374105052742E-18,-5.60383084497445E-34,
1.)) ;
#61827=DIRECTION('ref_axis',(0.707106781186548,-0.707106781186548,1.7845544107868E-18)) ;
#61828=DIRECTION('center_axis',(0.,0.,1.)) ;
#61829=DIRECTION('ref_axis',(0.,-1.,0.)) ;
#61830=DIRECTION('center_axis',(0.461352736642031,0.887216801234573,0.)) ;
#61831=DIRECTION('ref_axis',(0.887216801234573,-0.461352736642031,0.)) ;
#61832=DIRECTION('center_axis',(-0.887216801234586,-0.461352736642007,0.)) ;
#61833=DIRECTION('ref_axis',(0.461352736642007,-0.887216801234586,0.)) ;
#61834=DIRECTION('center_axis',(0.,0.,1.)) ;
#61835=DIRECTION('ref_axis',(0.707106781186547,-0.707106781186547,0.)) ;
#61836=DIRECTION('',(0.,0.,1.)) ;
#61837=DIRECTION('',(0.,0.,-1.)) ;
#61838=DIRECTION('center_axis',(-0.816496580927736,0.408248290463809,-0.408248290463898)) ;
#61839=DIRECTION('ref_axis',(-0.577350269189577,-0.577350269189695,0.577350269189606)) ;
#61840=DIRECTION('center_axis',(0.,-1.,0.)) ;
#61841=DIRECTION('ref_axis',(-1.,0.,0.)) ;
#61842=DIRECTION('center_axis',(0.,0.,1.)) ;
#61843=DIRECTION('ref_axis',(0.,-1.,0.)) ;
#61844=DIRECTION('center_axis',(-1.,0.,0.)) ;
#61845=DIRECTION('ref_axis',(0.,0.,1.)) ;
#61846=DIRECTION('center_axis',(0.,0.,-1.)) ;
#61847=DIRECTION('ref_axis',(0.,-1.,0.)) ;
#61848=DIRECTION('center_axis',(-0.82858896869141,0.559857411278002,0.)) ;
#61849=DIRECTION('ref_axis',(0.559857411278002,0.82858896869141,0.)) ;
#61850=DIRECTION('center_axis',(-0.82858896869141,0.559857411278002,0.)) ;
#61851=DIRECTION('ref_axis',(0.559857411278002,0.82858896869141,0.)) ;
#61852=DIRECTION('center_axis',(0.559857411277957,-0.82858896869144,0.)) ;
#61853=DIRECTION('ref_axis',(0.82858896869144,0.559857411277957,0.)) ;
#61854=DIRECTION('center_axis',(0.559857411277957,-0.82858896869144,0.)) ;
#61855=DIRECTION('ref_axis',(0.82858896869144,0.559857411277957,0.)) ;
#61856=DIRECTION('center_axis',(0.,0.,1.)) ;
#61857=DIRECTION('ref_axis',(-0.707106781186547,-0.707106781186547,0.)) ;
#61858=DIRECTION('',(0.,0.,1.)) ;
#61859=DIRECTION('',(0.,0.,-1.)) ;
#61860=DIRECTION('center_axis',(1.,0.,2.52374105052742E-18)) ;
#61861=DIRECTION('ref_axis',(-1.7845544107868E-18,-0.707106781186547,0.707106781186547)) ;
#61862=DIRECTION('',(-1.,0.,-2.52374105052742E-18)) ;
#61863=DIRECTION('',(1.,0.,2.52374105052742E-18)) ;
#61864=DIRECTION('center_axis',(0.,0.,-1.)) ;
#61865=DIRECTION('ref_axis',(-1.,0.,0.)) ;
#61866=DIRECTION('center_axis',(1.,0.,0.)) ;
#61867=DIRECTION('ref_axis',(0.,1.,0.)) ;
#61868=DIRECTION('center_axis',(0.,0.,-1.)) ;
#61869=DIRECTION('ref_axis',(-1.,0.,0.)) ;
#61870=DIRECTION('center_axis',(0.,1.,0.)) ;
#61871=DIRECTION('ref_axis',(0.,0.,1.)) ;
#61872=DIRECTION('center_axis',(-2.52374105052742E-18,-5.60383084497445E-34,
1.)) ;
#61873=DIRECTION('ref_axis',(-0.707106781186548,-0.707106781186548,-1.7845544107868E-18)) ;
#61874=DIRECTION('center_axis',(0.,0.,1.)) ;
#61875=DIRECTION('ref_axis',(-1.,0.,0.)) ;
#61876=DIRECTION('center_axis',(0.88721680123456,-0.461352736642057,0.)) ;
#61877=DIRECTION('ref_axis',(-0.461352736642057,-0.88721680123456,0.)) ;
#61878=DIRECTION('center_axis',(-0.461352736642031,0.887216801234573,0.)) ;
#61879=DIRECTION('ref_axis',(-0.887216801234573,-0.461352736642031,0.)) ;
#61880=DIRECTION('center_axis',(0.,0.,1.)) ;
#61881=DIRECTION('ref_axis',(-0.707106781186547,-0.707106781186547,0.)) ;
#61882=DIRECTION('',(0.,0.,1.)) ;
#61883=DIRECTION('',(0.,0.,-1.)) ;
#61884=DIRECTION('center_axis',(0.,0.,-1.)) ;
#61885=DIRECTION('ref_axis',(-1.,0.,0.)) ;
#61886=DIRECTION('center_axis',(-1.,0.,0.)) ;
#61887=DIRECTION('ref_axis',(0.,-1.,0.)) ;
#61888=DIRECTION('center_axis',(0.,0.,-1.)) ;
#61889=DIRECTION('ref_axis',(1.,0.,0.)) ;
#61890=DIRECTION('center_axis',(0.,-1.,0.)) ;
#61891=DIRECTION('ref_axis',(0.,0.,1.)) ;
#61892=DIRECTION('center_axis',(-2.52374105052742E-18,-5.60383084497445E-34,
1.)) ;
#61893=DIRECTION('ref_axis',(0.707106781186548,0.707106781186548,1.7845544107868E-18)) ;
#61894=DIRECTION('center_axis',(0.,0.,1.)) ;
#61895=DIRECTION('ref_axis',(1.,0.,0.)) ;
#61896=DIRECTION('center_axis',(-0.88721680123456,0.461352736642057,0.)) ;
#61897=DIRECTION('ref_axis',(0.461352736642057,0.88721680123456,0.)) ;
#61898=DIRECTION('center_axis',(0.461352736642031,-0.887216801234573,0.)) ;
#61899=DIRECTION('ref_axis',(0.887216801234573,0.461352736642031,0.)) ;
#61900=DIRECTION('center_axis',(0.,0.,1.)) ;
#61901=DIRECTION('ref_axis',(0.707106781186547,0.707106781186547,0.)) ;
#61902=DIRECTION('',(0.,0.,1.)) ;
#61903=DIRECTION('',(0.,0.,-1.)) ;
#61904=DIRECTION('center_axis',(1.41426179436738E-51,-1.,-5.60383084497445E-34)) ;
#61905=DIRECTION('ref_axis',(-0.707106781186547,-3.96250679110377E-34,0.707106781186547)) ;
#61906=DIRECTION('',(-1.41426179436738E-51,1.,5.60383084497445E-34)) ;
#61907=DIRECTION('',(1.41426179436738E-51,-1.,-5.60383084497445E-34)) ;
#61908=DIRECTION('center_axis',(-0.816496580927736,0.408248290463809,0.408248290463898)) ;
#61909=DIRECTION('ref_axis',(0.577350269189577,0.577350269189695,0.577350269189606)) ;
#61910=DIRECTION('center_axis',(0.,1.,0.)) ;
#61911=DIRECTION('ref_axis',(1.,0.,0.)) ;
#61912=DIRECTION('center_axis',(0.,0.,1.)) ;
#61913=DIRECTION('ref_axis',(0.,1.,0.)) ;
#61914=DIRECTION('center_axis',(1.,0.,0.)) ;
#61915=DIRECTION('ref_axis',(0.,0.,1.)) ;
#61916=DIRECTION('center_axis',(0.,0.,-1.)) ;
#61917=DIRECTION('ref_axis',(0.,1.,0.)) ;
#61918=DIRECTION('center_axis',(0.82858896869141,-0.559857411278002,0.)) ;
#61919=DIRECTION('ref_axis',(-0.559857411278002,-0.82858896869141,0.)) ;
#61920=DIRECTION('center_axis',(0.82858896869141,-0.559857411278002,0.)) ;
#61921=DIRECTION('ref_axis',(-0.559857411278002,-0.82858896869141,0.)) ;
#61922=DIRECTION('center_axis',(-0.559857411277957,0.82858896869144,0.)) ;
#61923=DIRECTION('ref_axis',(-0.82858896869144,-0.559857411277957,0.)) ;
#61924=DIRECTION('center_axis',(-0.559857411277957,0.82858896869144,0.)) ;
#61925=DIRECTION('ref_axis',(-0.82858896869144,-0.559857411277957,0.)) ;
#61926=DIRECTION('center_axis',(0.,0.,1.)) ;
#61927=DIRECTION('ref_axis',(0.707106781186547,0.707106781186547,0.)) ;
#61928=DIRECTION('',(0.,0.,1.)) ;
#61929=DIRECTION('',(0.,0.,-1.)) ;
#61930=DIRECTION('center_axis',(0.,0.,-1.)) ;
#61931=DIRECTION('ref_axis',(-1.,0.,0.)) ;
#61932=DIRECTION('center_axis',(0.,-1.,0.)) ;
#61933=DIRECTION('ref_axis',(1.,0.,0.)) ;
#61934=DIRECTION('center_axis',(0.,0.,-1.)) ;
#61935=DIRECTION('ref_axis',(0.,1.,0.)) ;
#61936=DIRECTION('center_axis',(1.,0.,0.)) ;
#61937=DIRECTION('ref_axis',(0.,0.,1.)) ;
#61938=DIRECTION('center_axis',(-2.52374105052742E-18,-5.60383084497445E-34,
1.)) ;
#61939=DIRECTION('ref_axis',(-0.707106781186548,0.707106781186548,-1.7845544107868E-18)) ;
#61940=DIRECTION('center_axis',(0.,0.,1.)) ;
#61941=DIRECTION('ref_axis',(0.,1.,0.)) ;
#61942=DIRECTION('center_axis',(-0.461352736642031,-0.887216801234573,0.)) ;
#61943=DIRECTION('ref_axis',(-0.887216801234573,0.461352736642031,0.)) ;
#61944=DIRECTION('center_axis',(0.887216801234586,0.461352736642007,0.)) ;
#61945=DIRECTION('ref_axis',(-0.461352736642007,0.887216801234586,0.)) ;
#61946=DIRECTION('center_axis',(0.,0.,1.)) ;
#61947=DIRECTION('ref_axis',(-0.707106781186547,0.707106781186547,0.)) ;
#61948=DIRECTION('',(0.,0.,1.)) ;
#61949=DIRECTION('',(0.,0.,-1.)) ;
#61950=DIRECTION('center_axis',(1.,0.,2.52374105052742E-18)) ;
#61951=DIRECTION('ref_axis',(-1.7845544107868E-18,-0.707106781186547,0.707106781186547)) ;
#61952=DIRECTION('',(-1.,0.,-2.52374105052742E-18)) ;
#61953=DIRECTION('',(1.,0.,2.52374105052742E-18)) ;
#61954=DIRECTION('center_axis',(0.,0.,-1.)) ;
#61955=DIRECTION('ref_axis',(-1.,0.,0.)) ;
#61956=DIRECTION('center_axis',(1.,0.,0.)) ;
#61957=DIRECTION('ref_axis',(0.,1.,0.)) ;
#61958=DIRECTION('center_axis',(0.,0.,-1.)) ;
#61959=DIRECTION('ref_axis',(-1.,0.,0.)) ;
#61960=DIRECTION('center_axis',(0.,1.,0.)) ;
#61961=DIRECTION('ref_axis',(0.,0.,1.)) ;
#61962=DIRECTION('center_axis',(-2.52374105052742E-18,-5.60383084497445E-34,
1.)) ;
#61963=DIRECTION('ref_axis',(-0.707106781186521,-0.707106781186574,-1.78455441078673E-18)) ;
#61964=DIRECTION('center_axis',(0.,0.,1.)) ;
#61965=DIRECTION('ref_axis',(-1.,0.,0.)) ;
#61966=DIRECTION('center_axis',(0.88721680123456,-0.461352736642057,0.)) ;
#61967=DIRECTION('ref_axis',(-0.461352736642057,-0.88721680123456,0.)) ;
#61968=DIRECTION('center_axis',(-0.461352736642031,0.887216801234573,0.)) ;
#61969=DIRECTION('ref_axis',(-0.887216801234573,-0.461352736642031,0.)) ;
#61970=DIRECTION('center_axis',(0.,0.,1.)) ;
#61971=DIRECTION('ref_axis',(-0.707106781186495,-0.7071067811866,0.)) ;
#61972=DIRECTION('',(0.,0.,1.)) ;
#61973=DIRECTION('',(0.,0.,-1.)) ;
#61974=DIRECTION('center_axis',(-0.816496580927736,-0.408248290463809,0.408248290463898)) ;
#61975=DIRECTION('ref_axis',(0.577350269189577,-0.577350269189695,0.577350269189606)) ;
#61976=DIRECTION('center_axis',(1.,0.,0.)) ;
#61977=DIRECTION('ref_axis',(0.,-1.,0.)) ;
#61978=DIRECTION('center_axis',(0.,0.,1.)) ;
#61979=DIRECTION('ref_axis',(1.,0.,0.)) ;
#61980=DIRECTION('center_axis',(0.,-1.,0.)) ;
#61981=DIRECTION('ref_axis',(0.,0.,1.)) ;
#61982=DIRECTION('center_axis',(0.,0.,-1.)) ;
#61983=DIRECTION('ref_axis',(1.,0.,0.)) ;
#61984=DIRECTION('center_axis',(-0.559857411277938,-0.828588968691453,0.)) ;
#61985=DIRECTION('ref_axis',(-0.828588968691453,0.559857411277938,0.)) ;
#61986=DIRECTION('center_axis',(-0.559857411277938,-0.828588968691453,0.)) ;
#61987=DIRECTION('ref_axis',(-0.828588968691453,0.559857411277938,0.)) ;
#61988=DIRECTION('center_axis',(0.82858896869141,0.559857411278002,0.)) ;
#61989=DIRECTION('ref_axis',(-0.559857411278002,0.82858896869141,0.)) ;
#61990=DIRECTION('center_axis',(0.82858896869141,0.559857411278002,0.)) ;
#61991=DIRECTION('ref_axis',(-0.559857411278002,0.82858896869141,0.)) ;
#61992=DIRECTION('center_axis',(0.,0.,1.)) ;
#61993=DIRECTION('ref_axis',(0.707106781186547,-0.707106781186547,0.)) ;
#61994=DIRECTION('',(0.,0.,1.)) ;
#61995=DIRECTION('',(0.,0.,-1.)) ;
#61996=DIRECTION('center_axis',(-1.41426179436738E-51,1.,5.60383084497445E-34)) ;
#61997=DIRECTION('ref_axis',(0.707106781186547,-3.96250679110377E-34,0.707106781186547)) ;
#61998=DIRECTION('',(1.41426179436738E-51,-1.,-5.60383084497445E-34)) ;
#61999=DIRECTION('',(-1.41426179436738E-51,1.,5.60383084497445E-34)) ;
#62000=DIRECTION('center_axis',(0.,0.,-1.)) ;
#62001=DIRECTION('ref_axis',(-1.,0.,0.)) ;
#62002=DIRECTION('center_axis',(0.,-1.,0.)) ;
#62003=DIRECTION('ref_axis',(1.,0.,0.)) ;
#62004=DIRECTION('center_axis',(0.,0.,-1.)) ;
#62005=DIRECTION('ref_axis',(0.,1.,0.)) ;
#62006=DIRECTION('center_axis',(1.,0.,0.)) ;
#62007=DIRECTION('ref_axis',(0.,0.,1.)) ;
#62008=DIRECTION('center_axis',(-2.52374105052742E-18,-5.60383084497445E-34,
1.)) ;
#62009=DIRECTION('ref_axis',(-0.707106781186548,0.707106781186548,-1.7845544107868E-18)) ;
#62010=DIRECTION('center_axis',(0.,0.,1.)) ;
#62011=DIRECTION('ref_axis',(0.,1.,0.)) ;
#62012=DIRECTION('center_axis',(-0.461352736642031,-0.887216801234573,0.)) ;
#62013=DIRECTION('ref_axis',(-0.887216801234573,0.461352736642031,0.)) ;
#62014=DIRECTION('center_axis',(0.887216801234586,0.461352736642007,0.)) ;
#62015=DIRECTION('ref_axis',(-0.461352736642007,0.887216801234586,0.)) ;
#62016=DIRECTION('center_axis',(0.,0.,1.)) ;
#62017=DIRECTION('ref_axis',(-0.707106781186547,0.707106781186547,0.)) ;
#62018=DIRECTION('',(0.,0.,1.)) ;
#62019=DIRECTION('',(0.,0.,-1.)) ;
#62020=DIRECTION('center_axis',(1.,0.,2.52374105052742E-18)) ;
#62021=DIRECTION('ref_axis',(-1.7845544107868E-18,-0.707106781186547,0.707106781186547)) ;
#62022=DIRECTION('',(-1.,0.,-2.52374105052742E-18)) ;
#62023=DIRECTION('',(1.,0.,2.52374105052742E-18)) ;
#62024=DIRECTION('center_axis',(-1.41426179436738E-51,1.,5.60383084497445E-34)) ;
#62025=DIRECTION('ref_axis',(0.707106781186495,-3.96250679110407E-34,0.7071067811866)) ;
#62026=DIRECTION('',(1.41426179436738E-51,-1.,-5.60383084497445E-34)) ;
#62027=DIRECTION('',(-1.41426179436738E-51,1.,5.60383084497445E-34)) ;
#62028=DIRECTION('center_axis',(-1.,0.,-2.52374105052742E-18)) ;
#62029=DIRECTION('ref_axis',(-1.7845544107868E-18,0.707106781186547,0.707106781186547)) ;
#62030=DIRECTION('',(1.,0.,2.52374105052742E-18)) ;
#62031=DIRECTION('',(-1.,0.,-2.52374105052742E-18)) ;
#62032=DIRECTION('center_axis',(-1.41426179436738E-51,1.,5.60383084497445E-34)) ;
#62033=DIRECTION('ref_axis',(0.707106781186547,-3.96250679110377E-34,0.707106781186547)) ;
#62034=DIRECTION('',(1.41426179436738E-51,-1.,-5.60383084497445E-34)) ;
#62035=DIRECTION('',(-1.41426179436738E-51,1.,5.60383084497445E-34)) ;
#62036=DIRECTION('center_axis',(-1.,0.,-2.52374105052742E-18)) ;
#62037=DIRECTION('ref_axis',(-1.7845544107868E-18,0.707106781186547,0.707106781186547)) ;
#62038=DIRECTION('',(1.,0.,2.52374105052742E-18)) ;
#62039=DIRECTION('',(-1.,0.,-2.52374105052742E-18)) ;
#62040=DIRECTION('center_axis',(1.41426179436738E-51,-1.,-5.60383084497445E-34)) ;
#62041=DIRECTION('ref_axis',(-0.707106781186547,-3.96250679110377E-34,0.707106781186547)) ;
#62042=DIRECTION('',(-1.41426179436738E-51,1.,5.60383084497445E-34)) ;
#62043=DIRECTION('',(1.41426179436738E-51,-1.,-5.60383084497445E-34)) ;
#62044=DIRECTION('center_axis',(-1.,0.,-2.52374105052742E-18)) ;
#62045=DIRECTION('ref_axis',(-1.7845544107868E-18,0.707106781186547,0.707106781186547)) ;
#62046=DIRECTION('',(1.,0.,2.52374105052742E-18)) ;
#62047=DIRECTION('',(-1.,0.,-2.52374105052742E-18)) ;
#62048=DIRECTION('center_axis',(-1.,-1.41426179436738E-51,0.)) ;
#62049=DIRECTION('ref_axis',(1.41426179436738E-51,-1.,-5.60383084497445E-34)) ;
#62050=DIRECTION('',(-1.41426179436738E-51,1.,0.)) ;
#62051=DIRECTION('center_axis',(0.,-1.,0.)) ;
#62052=DIRECTION('ref_axis',(1.,0.,2.52374105052742E-18)) ;
#62053=DIRECTION('',(-1.,0.,0.)) ;
#62054=DIRECTION('center_axis',(1.,0.,0.)) ;
#62055=DIRECTION('ref_axis',(0.,0.707106781186535,-0.70710678118656)) ;
#62056=DIRECTION('',(1.,0.,0.)) ;
#62057=DIRECTION('center_axis',(-1.,-1.41426179436738E-51,0.)) ;
#62058=DIRECTION('ref_axis',(1.41426179436738E-51,-1.,-5.60383084497445E-34)) ;
#62059=DIRECTION('',(-1.41426179436738E-51,1.,0.)) ;
#62060=DIRECTION('center_axis',(1.41426179436738E-51,-1.,0.)) ;
#62061=DIRECTION('ref_axis',(0.707106781186585,1.00003410517028E-51,-0.70710678118651)) ;
#62062=DIRECTION('',(1.41426179436738E-51,-1.,0.)) ;
#62063=DIRECTION('center_axis',(0.,-1.,0.)) ;
#62064=DIRECTION('ref_axis',(1.,0.,2.52374105052742E-18)) ;
#62065=DIRECTION('',(-1.,0.,0.)) ;
#62066=DIRECTION('center_axis',(1.,0.,0.)) ;
#62067=DIRECTION('ref_axis',(0.,0.707106781186535,-0.70710678118656)) ;
#62068=DIRECTION('',(1.,0.,0.)) ;
#62069=DIRECTION('center_axis',(1.,1.41426179436738E-51,0.)) ;
#62070=DIRECTION('ref_axis',(-1.41426179436738E-51,1.,5.60383084497445E-34)) ;
#62071=DIRECTION('',(1.41426179436738E-51,-1.,0.)) ;
#62072=DIRECTION('center_axis',(-1.41426179436738E-51,1.,0.)) ;
#62073=DIRECTION('ref_axis',(-0.707106781186585,-1.00003410517028E-51,-0.70710678118651)) ;
#62074=DIRECTION('',(-1.41426179436738E-51,1.,0.)) ;
#62075=DIRECTION('center_axis',(0.,-1.,0.)) ;
#62076=DIRECTION('ref_axis',(1.,0.,2.52374105052742E-18)) ;
#62077=DIRECTION('',(-1.,0.,0.)) ;
#62078=DIRECTION('center_axis',(1.,0.,0.)) ;
#62079=DIRECTION('ref_axis',(0.,0.707106781186535,-0.70710678118656)) ;
#62080=DIRECTION('',(1.,0.,0.)) ;
#62081=DIRECTION('center_axis',(2.52374105052742E-18,5.60383084497445E-34,
-1.)) ;
#62082=DIRECTION('ref_axis',(1.,3.40207761657885E-68,2.52374105052742E-18)) ;
#62083=DIRECTION('center_axis',(2.52374105052742E-18,5.60383084497445E-34,
-1.)) ;
#62084=DIRECTION('ref_axis',(1.,7.00478855621806E-35,2.52374105052742E-18)) ;
#62085=DIRECTION('center_axis',(-1.,0.,0.)) ;
#62086=DIRECTION('ref_axis',(0.,-0.707106781186535,-0.70710678118656)) ;
#62087=DIRECTION('',(-1.,0.,0.)) ;
#62088=DIRECTION('',(1.,0.,0.)) ;
#62089=DIRECTION('center_axis',(-1.41426179436738E-51,1.,0.)) ;
#62090=DIRECTION('ref_axis',(-0.70710678118656,-1.00003410517025E-51,-0.707106781186535)) ;
#62091=DIRECTION('',(-1.41426179436738E-51,1.,0.)) ;
#62092=DIRECTION('',(1.41426179436738E-51,-1.,0.)) ;
#62093=DIRECTION('center_axis',(1.41426179436738E-51,-1.,0.)) ;
#62094=DIRECTION('ref_axis',(0.707106781186585,1.00003410517028E-51,-0.70710678118651)) ;
#62095=DIRECTION('',(1.41426179436738E-51,-1.,0.)) ;
#62096=DIRECTION('center_axis',(-1.,0.,0.)) ;
#62097=DIRECTION('ref_axis',(0.,-0.707106781186535,-0.70710678118656)) ;
#62098=DIRECTION('',(-1.,0.,0.)) ;
#62099=DIRECTION('',(1.,0.,0.)) ;
#62100=DIRECTION('center_axis',(1.41426179436738E-51,-1.,0.)) ;
#62101=DIRECTION('ref_axis',(0.707106781186585,1.00003410517028E-51,-0.70710678118651)) ;
#62102=DIRECTION('',(1.41426179436738E-51,-1.,0.)) ;
#62103=DIRECTION('',(-1.41426179436738E-51,1.,0.)) ;
#62104=DIRECTION('center_axis',(-1.,0.,0.)) ;
#62105=DIRECTION('ref_axis',(0.,-0.707106781186535,-0.70710678118656)) ;
#62106=DIRECTION('',(-1.,0.,0.)) ;
#62107=DIRECTION('',(1.,0.,0.)) ;
#62108=DIRECTION('center_axis',(-1.41426179436738E-51,1.,0.)) ;
#62109=DIRECTION('ref_axis',(-0.707106781186585,-1.00003410517028E-51,-0.70710678118651)) ;
#62110=DIRECTION('',(-1.41426179436738E-51,1.,0.)) ;
#62111=DIRECTION('',(1.41426179436738E-51,-1.,0.)) ;
#62112=DIRECTION('center_axis',(0.,1.,0.)) ;
#62113=DIRECTION('ref_axis',(-1.,0.,-2.52374105052742E-18)) ;
#62114=DIRECTION('center_axis',(-1.,-1.41426179436738E-51,0.)) ;
#62115=DIRECTION('ref_axis',(1.41426179436738E-51,-1.,-5.60383084497445E-34)) ;
#62116=DIRECTION('center_axis',(0.,1.,0.)) ;
#62117=DIRECTION('ref_axis',(-1.,0.,-2.52374105052742E-18)) ;
#62118=DIRECTION('center_axis',(1.,1.41426179436738E-51,0.)) ;
#62119=DIRECTION('ref_axis',(-1.41426179436738E-51,1.,5.60383084497445E-34)) ;
#62120=DIRECTION('center_axis',(0.,1.,0.)) ;
#62121=DIRECTION('ref_axis',(-1.,0.,-2.52374105052742E-18)) ;
#62122=DIRECTION('center_axis',(0.,0.,1.)) ;
#62123=DIRECTION('ref_axis',(1.,0.,0.)) ;
#62124=DIRECTION('center_axis',(-2.52374105052742E-18,-5.60383084497445E-34,
1.)) ;
#62125=DIRECTION('ref_axis',(1.,0.,0.)) ;
#62126=DIRECTION('center_axis',(0.,-1.,-5.60383084497445E-34)) ;
#62127=DIRECTION('ref_axis',(-1.,0.,0.)) ;
#62128=DIRECTION('center_axis',(-2.52374105052742E-18,-5.60383084497445E-34,
1.)) ;
#62129=DIRECTION('ref_axis',(1.,7.00478855621807E-35,2.52374105052742E-18)) ;
#62130=DIRECTION('center_axis',(0.,0.,1.)) ;
#62131=DIRECTION('ref_axis',(1.,0.,0.)) ;
#62132=DIRECTION('',(0.,0.,-1.)) ;
#62133=DIRECTION('center_axis',(2.52374105052742E-18,5.60383084497445E-34,
-1.)) ;
#62134=DIRECTION('ref_axis',(1.,-7.00478855621807E-35,2.52374105052742E-18)) ;
#62135=DIRECTION('center_axis',(2.52374105052742E-18,5.60383084497445E-34,
-1.)) ;
#62136=DIRECTION('ref_axis',(1.,-7.00478855621807E-35,2.52374105052742E-18)) ;
#62137=DIRECTION('center_axis',(2.52374105052742E-18,5.60383084497445E-34,
-1.)) ;
#62138=DIRECTION('ref_axis',(-1.,0.,0.)) ;
#62139=DIRECTION('center_axis',(-2.52374105052742E-18,-5.60383084497445E-34,
1.)) ;
#62140=DIRECTION('ref_axis',(1.,-7.00478855621806E-35,2.52374105052742E-18)) ;
#62141=DIRECTION('center_axis',(0.,-1.,-5.60383084497445E-34)) ;
#62142=DIRECTION('ref_axis',(1.,0.,0.)) ;
#62143=DIRECTION('center_axis',(2.52374105052742E-18,5.60383084497445E-34,
-1.)) ;
#62144=DIRECTION('ref_axis',(1.,3.40207761657885E-68,2.52374105052742E-18)) ;
#62145=DIRECTION('center_axis',(1.,1.41426179436738E-51,0.)) ;
#62146=DIRECTION('ref_axis',(-1.41426179436738E-51,1.,5.60383084497445E-34)) ;
#87531=CARTESIAN_POINT('',(0.,0.,0.)) ;
#87532=CARTESIAN_POINT('Origin',(82.08,243.620000000001,31.5013203435596)) ;
#87533=CARTESIAN_POINT('',(82.2,243.620000000001,31.5013203435596)) ;
#87534=CARTESIAN_POINT('',(82.32,243.620000000001,31.6213203435596)) ;
#87535=CARTESIAN_POINT('Origin',(82.32,243.620000000001,31.5013203435596)) ;
#87536=CARTESIAN_POINT('',(82.08,243.500000000001,31.5013203435596)) ;
#87537=CARTESIAN_POINT('Origin',(82.08,243.620000000001,31.5013203435596)) ;
#87538=CARTESIAN_POINT('',(82.08,243.380000000001,31.6213203435596)) ;
#87539=CARTESIAN_POINT('Origin',(82.08,243.380000000001,31.5013203435596)) ;
#87540=CARTESIAN_POINT('Origin',(82.08,243.620000000001,31.6213203435596)) ;
#87541=CARTESIAN_POINT('Ctrl Pts',(81.95,243.750000000001,30.9213203435596)) ;
#87542=CARTESIAN_POINT('Ctrl Pts',(82.0831487735147,243.68224032658,30.9213203435596)) ;
#87543=CARTESIAN_POINT('Ctrl Pts',(82.2022655046152,243.621718901757,31.0443420434627)) ;
#87544=CARTESIAN_POINT('Ctrl Pts',(82.1999288862301,243.62290611287,31.1751079336016)) ;
#87545=CARTESIAN_POINT('Ctrl Pts',(81.95,243.750000000001,30.9213203435596)) ;
#87546=CARTESIAN_POINT('Ctrl Pts',(82.0707400003391,243.669831553405,30.9213203435596)) ;
#87547=CARTESIAN_POINT('Ctrl Pts',(82.2034801642546,243.58435864747,31.023821296679)) ;
#87548=CARTESIAN_POINT('Ctrl Pts',(82.2008789356986,243.586033838743,31.1757084682768)) ;
#87549=CARTESIAN_POINT('Ctrl Pts',(81.95,243.750000000001,30.9213203435596)) ;
#87550=CARTESIAN_POINT('Ctrl Pts',(82.0489448986456,243.648036451712,30.9213203435596)) ;
#87551=CARTESIAN_POINT('Ctrl Pts',(82.1727418948934,243.51884959129,31.0059874513795)) ;
#87552=CARTESIAN_POINT('Ctrl Pts',(82.17031722008,243.521379708731,31.1762303714321)) ;
#87553=CARTESIAN_POINT('Ctrl Pts',(81.95,243.750000000001,30.9213203435596)) ;
#87554=CARTESIAN_POINT('Ctrl Pts',(82.027149796952,243.626241350018,30.9213203435596)) ;
#87555=CARTESIAN_POINT('Ctrl Pts',(82.1065333928586,243.496839168867,31.0290306789701)) ;
#87556=CARTESIAN_POINT('Ctrl Pts',(82.1049772902892,243.499375561169,31.1755560169681)) ;
#87557=CARTESIAN_POINT('Ctrl Pts',(81.95,243.750000000001,30.9213203435596)) ;
#87558=CARTESIAN_POINT('Ctrl Pts',(82.0177634684342,243.6168550215,30.9213203435596)) ;
#87559=CARTESIAN_POINT('Ctrl Pts',(82.0782935637655,243.497733002078,31.0443131727587)) ;
#87560=CARTESIAN_POINT('Ctrl Pts',(82.0771061831309,243.500069723277,31.1751087784957)) ;
#87561=CARTESIAN_POINT('',(82.08,243.500000000001,31.1713203435596)) ;
#87562=CARTESIAN_POINT('',(82.2,243.620000000001,31.1713203435596)) ;
#87563=CARTESIAN_POINT('Origin',(82.08,243.620000000001,31.1713203435596)) ;
#87564=CARTESIAN_POINT('',(81.95,243.750000000001,30.9213203435596)) ;
#87565=CARTESIAN_POINT('Origin',(81.95,243.750000000001,31.1713203435596)) ;
#87566=CARTESIAN_POINT('Origin',(81.95,243.750000000001,31.1713203435596)) ;
#87567=CARTESIAN_POINT('Origin',(82.08,243.620000000001,30.7213203435596)) ;
#87568=CARTESIAN_POINT('',(82.08,243.500000000001,30.7213203435596)) ;
#87569=CARTESIAN_POINT('',(82.2,243.620000000001,30.7213203435596)) ;
#87570=CARTESIAN_POINT('Origin',(81.22,243.380000000001,31.5013203435596)) ;
#87571=CARTESIAN_POINT('',(81.22,243.500000000001,31.5013203435596)) ;
#87572=CARTESIAN_POINT('',(81.22,243.380000000001,31.6213203435596)) ;
#87573=CARTESIAN_POINT('Origin',(81.22,243.380000000001,31.5013203435596)) ;
#87574=CARTESIAN_POINT('',(81.1,243.380000000001,31.5013203435596)) ;
#87575=CARTESIAN_POINT('Origin',(81.22,243.380000000001,31.5013203435596)) ;
#87576=CARTESIAN_POINT('Origin',(81.22,243.380000000001,31.5013203435596)) ;
#87577=CARTESIAN_POINT('Ctrl Pts',(80.85,243.750000000001,30.9213203435596)) ;
#87578=CARTESIAN_POINT('Ctrl Pts',(80.9060690286283,243.66694135397,30.9213203435596)) ;
#87579=CARTESIAN_POINT('Ctrl Pts',(81.0371686448867,243.472735445585,30.9670228859097)) ;
#87580=CARTESIAN_POINT('Ctrl Pts',(81.1000922423061,243.379647960366,31.096644359925)) ;
#87581=CARTESIAN_POINT('Ctrl Pts',(81.1000000308994,243.379784375592,31.1716078849273)) ;
#87582=CARTESIAN_POINT('Ctrl Pts',(80.85,243.750000000001,30.9213203435596)) ;
#87583=CARTESIAN_POINT('Ctrl Pts',(80.9112084395532,243.672080764895,30.9213203435596)) ;
#87584=CARTESIAN_POINT('Ctrl Pts',(81.0547714042485,243.489170469053,30.9800563984678)) ;
#87585=CARTESIAN_POINT('Ctrl Pts',(81.0999971368146,243.415654001957,31.1075891712013)) ;
#87586=CARTESIAN_POINT('Ctrl Pts',(81.0999308343166,243.415761752623,31.1715657892914)) ;
#87587=CARTESIAN_POINT('Ctrl Pts',(80.85,243.750000000001,30.9213203435596)) ;
#87588=CARTESIAN_POINT('Ctrl Pts',(80.9202050132824,243.681077338625,30.9213203435596)) ;
#87589=CARTESIAN_POINT('Ctrl Pts',(81.0858811028462,243.518463497089,30.9900089508676)) ;
#87590=CARTESIAN_POINT('Ctrl Pts',(81.1301864568706,243.478022835174,31.117002321391)) ;
#87591=CARTESIAN_POINT('Ctrl Pts',(81.1301214902666,243.478082140937,31.1715295882239)) ;
#87592=CARTESIAN_POINT('Ctrl Pts',(80.85,243.750000000001,30.9213203435596)) ;
#87593=CARTESIAN_POINT('Ctrl Pts',(80.9292015870114,243.690073912354,30.9213203435596)) ;
#87594=CARTESIAN_POINT('Ctrl Pts',(81.114823358716,243.549738586775,30.9767972196575)) ;
#87595=CARTESIAN_POINT('Ctrl Pts',(81.1933315389235,243.499977625037,31.1047490010866)) ;
#87596=CARTESIAN_POINT('Ctrl Pts',(81.1932164772698,243.500050566896,31.1715767127306)) ;
#87597=CARTESIAN_POINT('Ctrl Pts',(80.8500000000001,243.750000000001,30.9213203435596)) ;
#87598=CARTESIAN_POINT('Ctrl Pts',(80.9330587498157,243.693931075158,30.9213203435596)) ;
#87599=CARTESIAN_POINT('Ctrl Pts',(81.1272657467482,243.562830762151,30.9670226804587)) ;
#87600=CARTESIAN_POINT('Ctrl Pts',(81.2203527598548,243.499907763237,31.0966450170891)) ;
#87601=CARTESIAN_POINT('Ctrl Pts',(81.2202163453198,243.499999973768,31.1716078824025)) ;
#87602=CARTESIAN_POINT('',(81.1,243.380000000001,31.1713203435596)) ;
#87603=CARTESIAN_POINT('',(81.22,243.500000000001,31.1713203435596)) ;
#87604=CARTESIAN_POINT('Origin',(81.22,243.380000000001,31.1713203435596)) ;
#87605=CARTESIAN_POINT('',(81.0807585144051,243.594082084862,30.9758987384622)) ;
#87606=CARTESIAN_POINT('Origin',(80.85,243.750000000001,31.1713203435596)) ;
#87607=CARTESIAN_POINT('',(80.85,243.750000000001,30.9213203435596)) ;
#87608=CARTESIAN_POINT('Origin',(80.85,243.750000000001,31.1713203435596)) ;
#87609=CARTESIAN_POINT('',(81.0059179151387,243.519241485596,30.9758987384623)) ;
#87610=CARTESIAN_POINT('Origin',(80.85,243.750000000001,31.1713203435596)) ;
#87611=CARTESIAN_POINT('Origin',(80.85,243.750000000001,31.1713203435596)) ;
#87612=CARTESIAN_POINT('Origin',(81.22,243.380000000001,30.7213203435596)) ;
#87613=CARTESIAN_POINT('',(81.1,243.380000000001,30.7213203435596)) ;
#87614=CARTESIAN_POINT('',(81.22,243.500000000001,30.7213203435596)) ;
#87615=CARTESIAN_POINT('Origin',(82.08,243.980000000001,31.5013203435596)) ;
#87616=CARTESIAN_POINT('',(82.08,244.100000000001,31.5013203435596)) ;
#87617=CARTESIAN_POINT('',(82.08,244.220000000001,31.6213203435596)) ;
#87618=CARTESIAN_POINT('Origin',(82.08,244.220000000001,31.5013203435596)) ;
#87619=CARTESIAN_POINT('',(82.2,243.980000000001,31.5013203435596)) ;
#87620=CARTESIAN_POINT('Origin',(82.08,243.980000000001,31.5013203435596)) ;
#87621=CARTESIAN_POINT('',(82.32,243.980000000001,31.6213203435596)) ;
#87622=CARTESIAN_POINT('Origin',(82.32,243.980000000001,31.5013203435596)) ;
#87623=CARTESIAN_POINT('Origin',(82.08,243.980000000001,31.6213203435596)) ;
#87624=CARTESIAN_POINT('Ctrl Pts',(81.95,243.850000000001,30.9213203435596)) ;
#87625=CARTESIAN_POINT('Ctrl Pts',(82.0177596734215,243.983148773511,30.9213203435596)) ;
#87626=CARTESIAN_POINT('Ctrl Pts',(82.078281098242,244.102265504606,31.0443420434537)) ;
#87627=CARTESIAN_POINT('Ctrl Pts',(82.0770938871316,244.099928886226,31.175107933593)) ;
#87628=CARTESIAN_POINT('Ctrl Pts',(81.95,243.850000000001,30.9213203435596)) ;
#87629=CARTESIAN_POINT('Ctrl Pts',(82.030168446596,243.970740000336,30.9213203435596)) ;
#87630=CARTESIAN_POINT('Ctrl Pts',(82.1156413526764,244.103480164368,31.0238212966733)) ;
#87631=CARTESIAN_POINT('Ctrl Pts',(82.1139661614044,244.100878935816,31.1757084682668)) ;
#87632=CARTESIAN_POINT('Ctrl Pts',(81.95,243.850000000001,30.9213203435596)) ;
#87633=CARTESIAN_POINT('Ctrl Pts',(82.0519635482869,243.948944898645,30.9213203435596)) ;
#87634=CARTESIAN_POINT('Ctrl Pts',(82.1811504039019,244.072741890888,31.0059874513777)) ;
#87635=CARTESIAN_POINT('Ctrl Pts',(82.1786202865599,244.070317216158,31.1762303714208)) ;
#87636=CARTESIAN_POINT('Ctrl Pts',(81.95,243.850000000001,30.9213203435596)) ;
#87637=CARTESIAN_POINT('Ctrl Pts',(82.0737586499778,243.927149796954,30.9213203435596)) ;
#87638=CARTESIAN_POINT('Ctrl Pts',(82.20316083127,244.006533392985,31.0290306789624)) ;
#87639=CARTESIAN_POINT('Ctrl Pts',(82.2006244389709,244.004977290417,31.1755560169585)) ;
#87640=CARTESIAN_POINT('Ctrl Pts',(81.95,243.850000000001,30.9213203435596)) ;
#87641=CARTESIAN_POINT('Ctrl Pts',(82.0831449784942,243.917763468438,30.9213203435596)) ;
#87642=CARTESIAN_POINT('Ctrl Pts',(82.20226699791,243.97829356377,31.0443131727465)) ;
#87643=CARTESIAN_POINT('Ctrl Pts',(82.1999302767171,243.977106183138,31.1751087784873)) ;
#87644=CARTESIAN_POINT('',(82.2,243.980000000001,31.1713203435596)) ;
#87645=CARTESIAN_POINT('',(82.08,244.100000000001,31.1713203435596)) ;
#87646=CARTESIAN_POINT('Origin',(82.08,243.980000000001,31.1713203435596)) ;
#87647=CARTESIAN_POINT('',(81.95,243.850000000001,30.9213203435596)) ;
#87648=CARTESIAN_POINT('Origin',(81.95,243.850000000001,31.1713203435596)) ;
#87649=CARTESIAN_POINT('Origin',(81.95,243.850000000001,31.1713203435596)) ;
#87650=CARTESIAN_POINT('Origin',(82.08,243.980000000001,30.7213203435596)) ;
#87651=CARTESIAN_POINT('',(82.2,243.980000000001,30.7213203435596)) ;
#87652=CARTESIAN_POINT('',(82.08,244.100000000001,30.7213203435596)) ;
#87653=CARTESIAN_POINT('Origin',(82.32,243.950000000001,31.5013203435596)) ;
#87654=CARTESIAN_POINT('',(82.32,243.950000000001,31.6213203435596)) ;
#87655=CARTESIAN_POINT('',(82.2,243.950000000001,31.5013203435596)) ;
#87656=CARTESIAN_POINT('Origin',(80.98,242.520000000001,31.5013203435596)) ;
#87657=CARTESIAN_POINT('',(81.1,242.520000000001,31.5013203435596)) ;
#87658=CARTESIAN_POINT('',(81.22,242.520000000001,31.6213203435596)) ;
#87659=CARTESIAN_POINT('Origin',(81.22,242.520000000001,31.5013203435596)) ;
#87660=CARTESIAN_POINT('',(80.98,242.400000000001,31.5013203435596)) ;
#87661=CARTESIAN_POINT('Origin',(80.98,242.520000000001,31.5013203435596)) ;
#87662=CARTESIAN_POINT('',(80.98,242.280000000001,31.6213203435596)) ;
#87663=CARTESIAN_POINT('Origin',(80.98,242.280000000001,31.5013203435596)) ;
#87664=CARTESIAN_POINT('Origin',(80.98,242.520000000001,31.6213203435596)) ;
#87665=CARTESIAN_POINT('Ctrl Pts',(80.85,242.650000000001,30.9213203435596)) ;
#87666=CARTESIAN_POINT('Ctrl Pts',(80.9831487735423,242.582240326584,30.9213203435596)) ;
#87667=CARTESIAN_POINT('Ctrl Pts',(81.1022655046685,242.521718901747,31.0443420435114)) ;
#87668=CARTESIAN_POINT('Ctrl Pts',(81.0999288862541,242.522906112875,31.1751079336474)) ;
#87669=CARTESIAN_POINT('Ctrl Pts',(80.85,242.650000000001,30.9213203435596)) ;
#87670=CARTESIAN_POINT('Ctrl Pts',(80.9707400003613,242.569831553404,30.9213203435596)) ;
#87671=CARTESIAN_POINT('Ctrl Pts',(81.1034801636441,242.484358648257,31.0238212967098)) ;
#87672=CARTESIAN_POINT('Ctrl Pts',(81.1008789350685,242.486033839536,31.1757084683305)) ;
#87673=CARTESIAN_POINT('Ctrl Pts',(80.85,242.650000000001,30.9213203435596)) ;
#87674=CARTESIAN_POINT('Ctrl Pts',(80.9489448986537,242.548036451696,30.9213203435596)) ;
#87675=CARTESIAN_POINT('Ctrl Pts',(81.0727419165628,242.418849565278,31.0059874513892)) ;
#87676=CARTESIAN_POINT('Ctrl Pts',(81.070317241297,242.421379683257,31.1762303714928)) ;
#87677=CARTESIAN_POINT('Ctrl Pts',(80.85,242.650000000001,30.9213203435596)) ;
#87678=CARTESIAN_POINT('Ctrl Pts',(80.9271497969463,242.526241349989,30.9213203435596)) ;
#87679=CARTESIAN_POINT('Ctrl Pts',(81.0065333921819,242.396839169602,31.0290306790113)) ;
#87680=CARTESIAN_POINT('Ctrl Pts',(81.0049772896065,242.39937556192,31.1755560170196)) ;
#87681=CARTESIAN_POINT('Ctrl Pts',(80.8500000000001,242.650000000001,30.9213203435596)) ;
#87682=CARTESIAN_POINT('Ctrl Pts',(80.9177634684198,242.516855021462,30.9213203435596)) ;
#87683=CARTESIAN_POINT('Ctrl Pts',(80.9782935637477,242.39773300201,31.0443131728241)) ;
#87684=CARTESIAN_POINT('Ctrl Pts',(80.9771061830986,242.400069723238,31.175108778541)) ;
#87685=CARTESIAN_POINT('',(80.98,242.400000000001,31.1713203435596)) ;
#87686=CARTESIAN_POINT('',(81.1,242.520000000001,31.1713203435596)) ;
#87687=CARTESIAN_POINT('Origin',(80.98,242.520000000001,31.1713203435596)) ;
#87688=CARTESIAN_POINT('',(80.85,242.650000000001,30.9213203435596)) ;
#87689=CARTESIAN_POINT('Origin',(80.85,242.650000000001,31.1713203435596)) ;
#87690=CARTESIAN_POINT('Origin',(80.85,242.650000000001,31.1713203435596)) ;
#87691=CARTESIAN_POINT('Origin',(80.98,242.520000000001,30.7213203435596)) ;
#87692=CARTESIAN_POINT('',(80.98,242.400000000001,30.7213203435596)) ;
#87693=CARTESIAN_POINT('',(81.1,242.520000000001,30.7213203435596)) ;
#87694=CARTESIAN_POINT('Origin',(81.22,244.220000000001,31.5013203435596)) ;
#87695=CARTESIAN_POINT('',(81.1,244.220000000001,31.5013203435596)) ;
#87696=CARTESIAN_POINT('',(81.22,244.220000000001,31.6213203435596)) ;
#87697=CARTESIAN_POINT('Origin',(81.22,244.220000000001,31.5013203435596)) ;
#87698=CARTESIAN_POINT('',(81.22,244.100000000001,31.5013203435596)) ;
#87699=CARTESIAN_POINT('Origin',(81.22,244.220000000001,31.5013203435596)) ;
#87700=CARTESIAN_POINT('Origin',(81.22,244.220000000001,31.5013203435596)) ;
#87701=CARTESIAN_POINT('Ctrl Pts',(80.85,243.850000000001,30.9213203435596)) ;
#87702=CARTESIAN_POINT('Ctrl Pts',(80.933058642349,243.906069032311,30.9213203435596)) ;
#87703=CARTESIAN_POINT('Ctrl Pts',(81.1272644866058,244.037168619611,30.9670229231865)) ;
#87704=CARTESIAN_POINT('Ctrl Pts',(81.2203519977101,244.100092231335,31.0966443451774)) ;
#87705=CARTESIAN_POINT('Ctrl Pts',(81.2202155986979,244.100000030893,31.1716078506955)) ;
#87706=CARTESIAN_POINT('Ctrl Pts',(80.85,243.850000000001,30.9213203435596)) ;
#87707=CARTESIAN_POINT('Ctrl Pts',(80.9279192326513,243.911208442009,30.9213203435596)) ;
#87708=CARTESIAN_POINT('Ctrl Pts',(81.1108294721138,244.05477138239,30.9800563956)) ;
#87709=CARTESIAN_POINT('Ctrl Pts',(81.1843459682786,244.0999971372,31.1075891515919)) ;
#87710=CARTESIAN_POINT('Ctrl Pts',(81.1842382304091,244.099930842572,31.1715657600926)) ;
#87711=CARTESIAN_POINT('Ctrl Pts',(80.85,243.850000000001,30.9213203435596)) ;
#87712=CARTESIAN_POINT('Ctrl Pts',(80.9189226613762,243.920205013284,30.9213203435596)) ;
#87713=CARTESIAN_POINT('Ctrl Pts',(81.0815364284407,244.085881025253,30.9900088723548)) ;
#87714=CARTESIAN_POINT('Ctrl Pts',(81.1219771701419,244.130186459382,31.1170022964528)) ;
#87715=CARTESIAN_POINT('Ctrl Pts',(81.1219178713322,244.130121500405,31.1715295633574)) ;
#87716=CARTESIAN_POINT('Ctrl Pts',(80.85,243.850000000001,30.9213203435596)) ;
#87717=CARTESIAN_POINT('Ctrl Pts',(80.9099260901013,243.929201584559,30.9213203435596)) ;
#87718=CARTESIAN_POINT('Ctrl Pts',(81.0502613754307,244.114823285899,30.9767972170891)) ;
#87719=CARTESIAN_POINT('Ctrl Pts',(81.1000223723327,244.193331508108,31.1047489821795)) ;
#87720=CARTESIAN_POINT('Ctrl Pts',(81.099949439114,244.193216460102,31.1715766822281)) ;
#87721=CARTESIAN_POINT('Ctrl Pts',(80.85,243.850000000001,30.9213203435596)) ;
#87722=CARTESIAN_POINT('Ctrl Pts',(80.9060689285239,243.933058746136,30.9213203435596)) ;
#87723=CARTESIAN_POINT('Ctrl Pts',(81.0371692125707,244.127265678943,30.9670227177986)) ;
#87724=CARTESIAN_POINT('Ctrl Pts',(81.1000922257932,244.220352717941,31.0966450022337)) ;
#87725=CARTESIAN_POINT('Ctrl Pts',(81.1000000262267,244.220216319619,31.1716078481715)) ;
#87726=CARTESIAN_POINT('',(81.22,244.100000000001,31.1713203435596)) ;
#87727=CARTESIAN_POINT('',(81.1,244.220000000001,31.1713203435596)) ;
#87728=CARTESIAN_POINT('Origin',(81.22,244.220000000001,31.1713203435596)) ;
#87729=CARTESIAN_POINT('',(81.00591790761,244.080758503264,30.9758987324555)) ;
#87730=CARTESIAN_POINT('Origin',(80.85,243.850000000001,31.1713203435596)) ;
#87731=CARTESIAN_POINT('',(80.85,243.850000000001,30.9213203435596)) ;
#87732=CARTESIAN_POINT('Origin',(80.85,243.850000000001,31.1713203435596)) ;
#87733=CARTESIAN_POINT('',(81.0807585032626,244.005917907611,30.9758987324554)) ;
#87734=CARTESIAN_POINT('Origin',(80.85,243.850000000001,31.1713203435596)) ;
#87735=CARTESIAN_POINT('Origin',(80.85,243.850000000001,31.1713203435596)) ;
#87736=CARTESIAN_POINT('Origin',(81.22,244.220000000001,30.7213203435596)) ;
#87737=CARTESIAN_POINT('',(81.22,244.100000000001,30.7213203435596)) ;
#87738=CARTESIAN_POINT('',(81.1,244.220000000001,30.7213203435596)) ;
#87739=CARTESIAN_POINT('Origin',(80.95,244.220000000001,31.5013203435596)) ;
#87740=CARTESIAN_POINT('',(80.95,244.220000000001,31.6213203435596)) ;
#87741=CARTESIAN_POINT('',(80.95,244.100000000001,31.5013203435596)) ;
#87742=CARTESIAN_POINT('Origin',(80.62,242.520000000001,31.5013203435596)) ;
#87743=CARTESIAN_POINT('',(80.62,242.400000000001,31.5013203435596)) ;
#87744=CARTESIAN_POINT('',(80.62,242.280000000001,31.6213203435596)) ;
#87745=CARTESIAN_POINT('Origin',(80.62,242.280000000001,31.5013203435596)) ;
#87746=CARTESIAN_POINT('',(80.5,242.520000000001,31.5013203435596)) ;
#87747=CARTESIAN_POINT('Origin',(80.62,242.520000000001,31.5013203435596)) ;
#87748=CARTESIAN_POINT('',(80.38,242.520000000001,31.6213203435596)) ;
#87749=CARTESIAN_POINT('Origin',(80.38,242.520000000001,31.5013203435596)) ;
#87750=CARTESIAN_POINT('Origin',(80.62,242.520000000001,31.6213203435596)) ;
#87751=CARTESIAN_POINT('Ctrl Pts',(80.75,242.650000000001,30.9213203435596)) ;
#87752=CARTESIAN_POINT('Ctrl Pts',(80.682240326584,242.516851226453,30.9213203435596)) ;
#87753=CARTESIAN_POINT('Ctrl Pts',(80.6217189017438,242.397734495321,31.0443420435221)) ;
#87754=CARTESIAN_POINT('Ctrl Pts',(80.6229061128752,242.400071113742,31.1751079336573)) ;
#87755=CARTESIAN_POINT('Ctrl Pts',(80.75,242.650000000001,30.9213203435596)) ;
#87756=CARTESIAN_POINT('Ctrl Pts',(80.6698315534017,242.529259999635,30.9213203435596)) ;
#87757=CARTESIAN_POINT('Ctrl Pts',(80.5843586484258,242.396519836488,31.0238212967164)) ;
#87758=CARTESIAN_POINT('Ctrl Pts',(80.5860338397051,242.399121065068,31.1757084683422)) ;
#87759=CARTESIAN_POINT('Ctrl Pts',(80.75,242.650000000001,30.9213203435596)) ;
#87760=CARTESIAN_POINT('Ctrl Pts',(80.6480364516902,242.551055101347,30.9213203435596)) ;
#87761=CARTESIAN_POINT('Ctrl Pts',(80.5188495596748,242.427258078776,31.0059874513904)) ;
#87762=CARTESIAN_POINT('Ctrl Pts',(80.5213796777706,242.42968275414,31.176230371506)) ;
#87763=CARTESIAN_POINT('Ctrl Pts',(80.75,242.650000000001,30.9213203435596)) ;
#87764=CARTESIAN_POINT('Ctrl Pts',(80.6262413499785,242.572850203058,30.9213203435596)) ;
#87765=CARTESIAN_POINT('Ctrl Pts',(80.4968391697564,242.493466607971,31.0290306790226)) ;
#87766=CARTESIAN_POINT('Ctrl Pts',(80.4993755620784,242.495022710548,31.1755560170308)) ;
#87767=CARTESIAN_POINT('Ctrl Pts',(80.75,242.650000000001,30.9213203435596)) ;
#87768=CARTESIAN_POINT('Ctrl Pts',(80.616855021449,242.582236531587,30.9213203435596)) ;
#87769=CARTESIAN_POINT('Ctrl Pts',(80.497733001995,242.521706436267,31.0443131728438)) ;
#87770=CARTESIAN_POINT('Ctrl Pts',(80.5000697232289,242.522893816919,31.1751087785507)) ;
#87771=CARTESIAN_POINT('',(80.5,242.520000000001,31.1713203435596)) ;
#87772=CARTESIAN_POINT('',(80.62,242.400000000001,31.1713203435596)) ;
#87773=CARTESIAN_POINT('Origin',(80.62,242.520000000001,31.1713203435596)) ;
#87774=CARTESIAN_POINT('',(80.75,242.650000000001,30.9213203435596)) ;
#87775=CARTESIAN_POINT('Origin',(80.75,242.650000000001,31.1713203435596)) ;
#87776=CARTESIAN_POINT('Origin',(80.75,242.650000000001,31.1713203435596)) ;
#87777=CARTESIAN_POINT('Origin',(80.62,242.520000000001,30.7213203435596)) ;
#87778=CARTESIAN_POINT('',(80.5,242.520000000001,30.7213203435596)) ;
#87779=CARTESIAN_POINT('',(80.62,242.400000000001,30.7213203435596)) ;
#87780=CARTESIAN_POINT('Origin',(80.98,245.080000000001,31.5013203435596)) ;
#87781=CARTESIAN_POINT('',(80.98,245.200000000001,31.5013203435596)) ;
#87782=CARTESIAN_POINT('',(80.98,245.320000000001,31.6213203435596)) ;
#87783=CARTESIAN_POINT('Origin',(80.98,245.320000000001,31.5013203435596)) ;
#87784=CARTESIAN_POINT('',(81.1,245.080000000001,31.5013203435596)) ;
#87785=CARTESIAN_POINT('Origin',(80.98,245.080000000001,31.5013203435596)) ;
#87786=CARTESIAN_POINT('',(81.22,245.080000000001,31.6213203435596)) ;
#87787=CARTESIAN_POINT('Origin',(81.22,245.080000000001,31.5013203435596)) ;
#87788=CARTESIAN_POINT('Origin',(80.98,245.080000000001,31.6213203435596)) ;
#87789=CARTESIAN_POINT('Ctrl Pts',(80.85,244.950000000001,30.9213203435596)) ;
#87790=CARTESIAN_POINT('Ctrl Pts',(80.9177596734216,245.083148773511,30.9213203435596)) ;
#87791=CARTESIAN_POINT('Ctrl Pts',(80.9782810982421,245.202265504606,31.0443420434537)) ;
#87792=CARTESIAN_POINT('Ctrl Pts',(80.9770938871316,245.199928886227,31.175107933593)) ;
#87793=CARTESIAN_POINT('Ctrl Pts',(80.85,244.950000000001,30.9213203435596)) ;
#87794=CARTESIAN_POINT('Ctrl Pts',(80.9301684465961,245.070740000336,30.9213203435596)) ;
#87795=CARTESIAN_POINT('Ctrl Pts',(81.0156413526763,245.203480164368,31.0238212966733)) ;
#87796=CARTESIAN_POINT('Ctrl Pts',(81.0139661614043,245.200878935816,31.1757084682668)) ;
#87797=CARTESIAN_POINT('Ctrl Pts',(80.85,244.950000000001,30.9213203435596)) ;
#87798=CARTESIAN_POINT('Ctrl Pts',(80.9519635482881,245.048944898644,30.9213203435596)) ;
#87799=CARTESIAN_POINT('Ctrl Pts',(81.0811504039054,245.172741890886,31.0059874513767)) ;
#87800=CARTESIAN_POINT('Ctrl Pts',(81.0786202865633,245.170317216156,31.1762303714209)) ;
#87801=CARTESIAN_POINT('Ctrl Pts',(80.85,244.950000000001,30.9213203435596)) ;
#87802=CARTESIAN_POINT('Ctrl Pts',(80.9737586499801,245.027149796952,30.9213203435596)) ;
#87803=CARTESIAN_POINT('Ctrl Pts',(81.1031608312723,245.106533392978,31.0290306789648)) ;
#87804=CARTESIAN_POINT('Ctrl Pts',(81.1006244389731,245.10497729041,31.1755560169585)) ;
#87805=CARTESIAN_POINT('Ctrl Pts',(80.8499999999999,244.950000000001,30.9213203435596)) ;
#87806=CARTESIAN_POINT('Ctrl Pts',(80.9831449784976,245.017763468435,30.9213203435596)) ;
#87807=CARTESIAN_POINT('Ctrl Pts',(81.1022669979097,245.07829356376,31.0443131727521)) ;
#87808=CARTESIAN_POINT('Ctrl Pts',(81.0999302767169,245.077106183128,31.1751087784871)) ;
#87809=CARTESIAN_POINT('',(81.1,245.080000000001,31.1713203435596)) ;
#87810=CARTESIAN_POINT('',(80.98,245.200000000001,31.1713203435596)) ;
#87811=CARTESIAN_POINT('Origin',(80.98,245.080000000001,31.1713203435596)) ;
#87812=CARTESIAN_POINT('',(80.85,244.950000000001,30.9213203435596)) ;
#87813=CARTESIAN_POINT('Origin',(80.85,244.950000000001,31.1713203435596)) ;
#87814=CARTESIAN_POINT('Origin',(80.85,244.950000000001,31.1713203435596)) ;
#87815=CARTESIAN_POINT('Origin',(80.98,245.080000000001,30.7213203435596)) ;
#87816=CARTESIAN_POINT('',(81.1,245.080000000001,30.7213203435596)) ;
#87817=CARTESIAN_POINT('',(80.98,245.200000000001,30.7213203435596)) ;
#87818=CARTESIAN_POINT('Origin',(81.22,244.500000000001,31.5013203435596)) ;
#87819=CARTESIAN_POINT('',(81.22,244.500000000001,31.6213203435596)) ;
#87820=CARTESIAN_POINT('',(81.1,244.500000000001,31.5013203435596)) ;
#87821=CARTESIAN_POINT('Origin',(80.38,243.380000000001,31.5013203435596)) ;
#87822=CARTESIAN_POINT('',(80.5,243.380000000001,31.5013203435596)) ;
#87823=CARTESIAN_POINT('',(80.38,243.380000000001,31.6213203435596)) ;
#87824=CARTESIAN_POINT('Origin',(80.38,243.380000000001,31.5013203435596)) ;
#87825=CARTESIAN_POINT('',(80.38,243.500000000001,31.5013203435596)) ;
#87826=CARTESIAN_POINT('Origin',(80.38,243.380000000001,31.5013203435596)) ;
#87827=CARTESIAN_POINT('Origin',(80.38,243.380000000001,31.5013203435596)) ;
#87828=CARTESIAN_POINT('Ctrl Pts',(80.75,243.750000000001,30.9213203435596)) ;
#87829=CARTESIAN_POINT('Ctrl Pts',(80.6669413510771,243.693930974265,30.9213203435596)) ;
#87830=CARTESIAN_POINT('Ctrl Pts',(80.4727353923176,243.56283133526,30.9670228566277)) ;
#87831=CARTESIAN_POINT('Ctrl Pts',(80.3796479274324,243.499907749076,31.0966443715092)) ;
#87832=CARTESIAN_POINT('Ctrl Pts',(80.379784355394,243.499999969096,31.1716079118165)) ;
#87833=CARTESIAN_POINT('Ctrl Pts',(80.75,243.750000000001,30.9213203435596)) ;
#87834=CARTESIAN_POINT('Ctrl Pts',(80.6720807629661,243.688791562376,30.9213203435596)) ;
#87835=CARTESIAN_POINT('Ctrl Pts',(80.4891704228372,243.545228578582,30.9800564007202)) ;
#87836=CARTESIAN_POINT('Ctrl Pts',(80.4156539785755,243.500002863489,31.1075891866046)) ;
#87837=CARTESIAN_POINT('Ctrl Pts',(80.4157617392922,243.500069172168,31.1715658122273)) ;
#87838=CARTESIAN_POINT('Ctrl Pts',(80.75,243.750000000001,30.9213203435596)) ;
#87839=CARTESIAN_POINT('Ctrl Pts',(80.6810773386231,243.679794986719,30.9213203435596)) ;
#87840=CARTESIAN_POINT('Ctrl Pts',(80.5184634385883,243.514118836202,30.9900090125417)) ;
#87841=CARTESIAN_POINT('Ctrl Pts',(80.4780228393493,243.469813545103,31.1170023409801)) ;
#87842=CARTESIAN_POINT('Ctrl Pts',(80.4780821505742,243.469878517698,31.1715296077568)) ;
#87843=CARTESIAN_POINT('Ctrl Pts',(80.75,243.750000000001,30.9213203435596)) ;
#87844=CARTESIAN_POINT('Ctrl Pts',(80.69007391428,243.670798411063,30.9213203435596)) ;
#87845=CARTESIAN_POINT('Ctrl Pts',(80.5497385570857,243.485176584085,30.9767972216749)) ;
#87846=CARTESIAN_POINT('Ctrl Pts',(80.4999776229693,243.406668436871,31.1047490159384)) ;
#87847=CARTESIAN_POINT('Ctrl Pts',(80.5000505716157,243.406783509245,31.1715767366906)) ;
#87848=CARTESIAN_POINT('Ctrl Pts',(80.75,243.750000000001,30.9213203435596)) ;
#87849=CARTESIAN_POINT('Ctrl Pts',(80.6939310780478,243.666941247294,30.9213203435596)) ;
#87850=CARTESIAN_POINT('Ctrl Pts',(80.5628307422909,243.47273419999,30.9670226511274)) ;
#87851=CARTESIAN_POINT('Ctrl Pts',(80.499907754619,243.379647207222,31.0966450287582)) ;
#87852=CARTESIAN_POINT('Ctrl Pts',(80.4999999737621,243.379783634492,31.1716079092912)) ;
#87853=CARTESIAN_POINT('',(80.38,243.500000000001,31.1713203435596)) ;
#87854=CARTESIAN_POINT('',(80.5,243.380000000001,31.1713203435596)) ;
#87855=CARTESIAN_POINT('Origin',(80.38,243.380000000001,31.1713203435596)) ;
#87856=CARTESIAN_POINT('',(80.5940820789473,243.519241476843,30.9758987431808)) ;
#87857=CARTESIAN_POINT('Origin',(80.75,243.750000000001,31.1713203435596)) ;
#87858=CARTESIAN_POINT('',(80.75,243.750000000001,30.9213203435596)) ;
#87859=CARTESIAN_POINT('Origin',(80.75,243.750000000001,31.1713203435596)) ;
#87860=CARTESIAN_POINT('',(80.5192414768421,243.594082078948,30.9758987431808)) ;
#87861=CARTESIAN_POINT('Origin',(80.75,243.750000000001,31.1713203435596)) ;
#87862=CARTESIAN_POINT('Origin',(80.75,243.750000000001,31.1713203435596)) ;
#87863=CARTESIAN_POINT('Origin',(80.38,243.380000000001,30.7213203435596)) ;
#87864=CARTESIAN_POINT('',(80.38,243.500000000001,30.7213203435596)) ;
#87865=CARTESIAN_POINT('',(80.5,243.380000000001,30.7213203435596)) ;
#87866=CARTESIAN_POINT('Origin',(80.62,245.080000000001,31.5013203435596)) ;
#87867=CARTESIAN_POINT('',(80.5,245.080000000001,31.5013203435596)) ;
#87868=CARTESIAN_POINT('',(80.38,245.080000000001,31.6213203435596)) ;
#87869=CARTESIAN_POINT('Origin',(80.38,245.080000000001,31.5013203435596)) ;
#87870=CARTESIAN_POINT('',(80.62,245.200000000001,31.5013203435596)) ;
#87871=CARTESIAN_POINT('Origin',(80.62,245.080000000001,31.5013203435596)) ;
#87872=CARTESIAN_POINT('',(80.62,245.320000000001,31.6213203435596)) ;
#87873=CARTESIAN_POINT('Origin',(80.62,245.320000000001,31.5013203435596)) ;
#87874=CARTESIAN_POINT('Origin',(80.62,245.080000000001,31.6213203435596)) ;
#87875=CARTESIAN_POINT('Ctrl Pts',(80.75,244.950000000001,30.9213203435596)) ;
#87876=CARTESIAN_POINT('Ctrl Pts',(80.6168512264854,245.017759673422,30.9213203435596)) ;
#87877=CARTESIAN_POINT('Ctrl Pts',(80.497734495385,245.078281098245,31.0443420434625)) ;
#87878=CARTESIAN_POINT('Ctrl Pts',(80.50007111377,245.077093887132,31.1751079336014)) ;
#87879=CARTESIAN_POINT('Ctrl Pts',(80.75,244.950000000001,30.9213203435596)) ;
#87880=CARTESIAN_POINT('Ctrl Pts',(80.6292599996609,245.030168446598,30.9213203435596)) ;
#87881=CARTESIAN_POINT('Ctrl Pts',(80.4965198357456,245.115641352532,31.023821296679)) ;
#87882=CARTESIAN_POINT('Ctrl Pts',(80.4991210643014,245.113966161259,31.1757084682767)) ;
#87883=CARTESIAN_POINT('Ctrl Pts',(80.75,244.950000000001,30.9213203435596)) ;
#87884=CARTESIAN_POINT('Ctrl Pts',(80.6510551013544,245.051963548291,30.9213203435596)) ;
#87885=CARTESIAN_POINT('Ctrl Pts',(80.5272581051066,245.181150408713,31.0059874513795)) ;
#87886=CARTESIAN_POINT('Ctrl Pts',(80.52968277992,245.178620291272,31.176230371432)) ;
#87887=CARTESIAN_POINT('Ctrl Pts',(80.75,244.950000000001,30.9213203435596)) ;
#87888=CARTESIAN_POINT('Ctrl Pts',(80.6728502030479,245.073758649985,30.9213203435596)) ;
#87889=CARTESIAN_POINT('Ctrl Pts',(80.593466607141,245.203160831135,31.0290306789699)) ;
#87890=CARTESIAN_POINT('Ctrl Pts',(80.5950227097103,245.200624438833,31.175556016968)) ;
#87891=CARTESIAN_POINT('Ctrl Pts',(80.75,244.950000000001,30.9213203435596)) ;
#87892=CARTESIAN_POINT('Ctrl Pts',(80.6822365315657,245.083144978503,30.9213203435596)) ;
#87893=CARTESIAN_POINT('Ctrl Pts',(80.6217064362341,245.202266997924,31.0443131727584)) ;
#87894=CARTESIAN_POINT('Ctrl Pts',(80.6228938168687,245.199930276725,31.1751087784956)) ;
#87895=CARTESIAN_POINT('',(80.62,245.200000000001,31.1713203435596)) ;
#87896=CARTESIAN_POINT('',(80.5,245.080000000001,31.1713203435596)) ;
#87897=CARTESIAN_POINT('Origin',(80.62,245.080000000001,31.1713203435596)) ;
#87898=CARTESIAN_POINT('',(80.75,244.950000000001,30.9213203435596)) ;
#87899=CARTESIAN_POINT('Origin',(80.75,244.950000000001,31.1713203435596)) ;
#87900=CARTESIAN_POINT('Origin',(80.75,244.950000000001,31.1713203435596)) ;
#87901=CARTESIAN_POINT('Origin',(80.62,245.080000000001,30.7213203435596)) ;
#87902=CARTESIAN_POINT('',(80.62,245.200000000001,30.7213203435596)) ;
#87903=CARTESIAN_POINT('',(80.5,245.080000000001,30.7213203435596)) ;
#87904=CARTESIAN_POINT('Origin',(80.65,245.320000000001,31.5013203435596)) ;
#87905=CARTESIAN_POINT('',(80.65,245.320000000001,31.6213203435596)) ;
#87906=CARTESIAN_POINT('',(80.65,245.200000000001,31.5013203435596)) ;
#87907=CARTESIAN_POINT('Origin',(79.52,243.620000000001,31.5013203435596)) ;
#87908=CARTESIAN_POINT('',(79.52,243.500000000001,31.5013203435596)) ;
#87909=CARTESIAN_POINT('',(79.52,243.380000000001,31.6213203435596)) ;
#87910=CARTESIAN_POINT('Origin',(79.52,243.380000000001,31.5013203435596)) ;
#87911=CARTESIAN_POINT('',(79.4,243.620000000001,31.5013203435596)) ;
#87912=CARTESIAN_POINT('Origin',(79.52,243.620000000001,31.5013203435596)) ;
#87913=CARTESIAN_POINT('',(79.28,243.620000000001,31.6213203435596)) ;
#87914=CARTESIAN_POINT('Origin',(79.28,243.620000000001,31.5013203435596)) ;
#87915=CARTESIAN_POINT('Origin',(79.52,243.620000000001,31.6213203435596)) ;
#87916=CARTESIAN_POINT('Ctrl Pts',(79.65,243.750000000001,30.9213203435596)) ;
#87917=CARTESIAN_POINT('Ctrl Pts',(79.582240326584,243.616851226453,30.9213203435596)) ;
#87918=CARTESIAN_POINT('Ctrl Pts',(79.5217189017439,243.497734495321,31.0443420435221)) ;
#87919=CARTESIAN_POINT('Ctrl Pts',(79.5229061128752,243.500071113742,31.1751079336573)) ;
#87920=CARTESIAN_POINT('Ctrl Pts',(79.65,243.750000000001,30.9213203435596)) ;
#87921=CARTESIAN_POINT('Ctrl Pts',(79.5698315534018,243.629259999635,30.9213203435596)) ;
#87922=CARTESIAN_POINT('Ctrl Pts',(79.4843586484258,243.496519836488,31.0238212967164)) ;
#87923=CARTESIAN_POINT('Ctrl Pts',(79.4860338397051,243.499121065068,31.1757084683421)) ;
#87924=CARTESIAN_POINT('Ctrl Pts',(79.65,243.750000000001,30.9213203435596)) ;
#87925=CARTESIAN_POINT('Ctrl Pts',(79.5480364516901,243.651055101347,30.9213203435596)) ;
#87926=CARTESIAN_POINT('Ctrl Pts',(79.4188495596745,243.527258078776,31.0059874513903)) ;
#87927=CARTESIAN_POINT('Ctrl Pts',(79.4213796777703,243.52968275414,31.176230371506)) ;
#87928=CARTESIAN_POINT('Ctrl Pts',(79.65,243.750000000001,30.9213203435596)) ;
#87929=CARTESIAN_POINT('Ctrl Pts',(79.5262413499783,243.672850203058,30.9213203435596)) ;
#87930=CARTESIAN_POINT('Ctrl Pts',(79.3968391697563,243.593466607972,31.0290306790228)) ;
#87931=CARTESIAN_POINT('Ctrl Pts',(79.3993755620783,243.595022710549,31.1755560170307)) ;
#87932=CARTESIAN_POINT('Ctrl Pts',(79.65,243.750000000001,30.9213203435596)) ;
#87933=CARTESIAN_POINT('Ctrl Pts',(79.5168550214487,243.682236531589,30.9213203435596)) ;
#87934=CARTESIAN_POINT('Ctrl Pts',(79.3977330019951,243.621706436268,31.0443131728442)) ;
#87935=CARTESIAN_POINT('Ctrl Pts',(79.4000697232289,243.62289381692,31.1751087785507)) ;
#87936=CARTESIAN_POINT('',(79.4,243.620000000001,31.1713203435596)) ;
#87937=CARTESIAN_POINT('',(79.52,243.500000000001,31.1713203435596)) ;
#87938=CARTESIAN_POINT('Origin',(79.52,243.620000000001,31.1713203435596)) ;
#87939=CARTESIAN_POINT('',(79.65,243.750000000001,30.9213203435596)) ;
#87940=CARTESIAN_POINT('Origin',(79.65,243.750000000001,31.1713203435596)) ;
#87941=CARTESIAN_POINT('Origin',(79.65,243.750000000001,31.1713203435596)) ;
#87942=CARTESIAN_POINT('Origin',(79.52,243.620000000001,30.7213203435596)) ;
#87943=CARTESIAN_POINT('',(79.4,243.620000000001,30.7213203435596)) ;
#87944=CARTESIAN_POINT('',(79.52,243.500000000001,30.7213203435596)) ;
#87945=CARTESIAN_POINT('Origin',(80.38,244.220000000001,31.5013203435596)) ;
#87946=CARTESIAN_POINT('',(80.38,244.100000000001,31.5013203435596)) ;
#87947=CARTESIAN_POINT('',(80.38,244.220000000001,31.6213203435596)) ;
#87948=CARTESIAN_POINT('Origin',(80.38,244.220000000001,31.5013203435596)) ;
#87949=CARTESIAN_POINT('',(80.5,244.220000000001,31.5013203435596)) ;
#87950=CARTESIAN_POINT('Origin',(80.38,244.220000000001,31.5013203435596)) ;
#87951=CARTESIAN_POINT('Origin',(80.38,244.220000000001,31.5013203435596)) ;
#87952=CARTESIAN_POINT('Ctrl Pts',(80.7500000000001,243.850000000001,30.9213203435596)) ;
#87953=CARTESIAN_POINT('Ctrl Pts',(80.6939309713718,243.933058646032,30.9213203435596)) ;
#87954=CARTESIAN_POINT('Ctrl Pts',(80.5628313551136,244.127264554417,30.9670228859096)) ;
#87955=CARTESIAN_POINT('Ctrl Pts',(80.4999077576942,244.220352039636,31.0966443599245)) ;
#87956=CARTESIAN_POINT('Ctrl Pts',(80.4999999691007,244.22021562441,31.1716078849265)) ;
#87957=CARTESIAN_POINT('Ctrl Pts',(80.75,243.850000000001,30.9213203435596)) ;
#87958=CARTESIAN_POINT('Ctrl Pts',(80.6887915604468,243.927919235107,30.9213203435596)) ;
#87959=CARTESIAN_POINT('Ctrl Pts',(80.5452285957518,244.110829530948,30.9800563984677)) ;
#87960=CARTESIAN_POINT('Ctrl Pts',(80.5000028631856,244.184345998044,31.1075891712008)) ;
#87961=CARTESIAN_POINT('Ctrl Pts',(80.5000691656834,244.184238247379,31.1715657892908)) ;
#87962=CARTESIAN_POINT('Ctrl Pts',(80.75,243.850000000001,30.9213203435596)) ;
#87963=CARTESIAN_POINT('Ctrl Pts',(80.6797949867176,243.918922661378,30.9213203435596)) ;
#87964=CARTESIAN_POINT('Ctrl Pts',(80.5141188971542,244.081536502913,30.9900089508675)) ;
#87965=CARTESIAN_POINT('Ctrl Pts',(80.4698135431297,244.121977164828,31.1170023213905)) ;
#87966=CARTESIAN_POINT('Ctrl Pts',(80.4698785097335,244.121917859065,31.1715295882234)) ;
#87967=CARTESIAN_POINT('Ctrl Pts',(80.75,243.850000000001,30.9213203435596)) ;
#87968=CARTESIAN_POINT('Ctrl Pts',(80.6707984129886,243.909926087649,30.9213203435596)) ;
#87969=CARTESIAN_POINT('Ctrl Pts',(80.4851766412845,244.050261413227,30.9767972196575)) ;
#87970=CARTESIAN_POINT('Ctrl Pts',(80.4066684610771,244.100022374965,31.1047490010863)) ;
#87971=CARTESIAN_POINT('Ctrl Pts',(80.4067835227305,244.099949433106,31.17157671273)) ;
#87972=CARTESIAN_POINT('Ctrl Pts',(80.75,243.850000000001,30.9213203435596)) ;
#87973=CARTESIAN_POINT('Ctrl Pts',(80.6669412501844,243.906068924844,30.9213203435596)) ;
#87974=CARTESIAN_POINT('Ctrl Pts',(80.4727342532524,244.037169237852,30.9670226804588)) ;
#87975=CARTESIAN_POINT('Ctrl Pts',(80.3796472401461,244.100092236764,31.0966450170888)) ;
#87976=CARTESIAN_POINT('Ctrl Pts',(80.3797836546807,244.100000026234,31.1716078824018)) ;
#87977=CARTESIAN_POINT('',(80.5,244.220000000001,31.1713203435596)) ;
#87978=CARTESIAN_POINT('',(80.38,244.100000000001,31.1713203435596)) ;
#87979=CARTESIAN_POINT('Origin',(80.38,244.220000000001,31.1713203435596)) ;
#87980=CARTESIAN_POINT('',(80.5192414855947,244.00591791514,30.9758987384623)) ;
#87981=CARTESIAN_POINT('Origin',(80.75,243.850000000001,31.1713203435596)) ;
#87982=CARTESIAN_POINT('',(80.75,243.850000000001,30.9213203435596)) ;
#87983=CARTESIAN_POINT('Origin',(80.75,243.850000000001,31.1713203435596)) ;
#87984=CARTESIAN_POINT('',(80.5940820848613,244.080758514406,30.9758987384623)) ;
#87985=CARTESIAN_POINT('Origin',(80.75,243.850000000001,31.1713203435596)) ;
#87986=CARTESIAN_POINT('Origin',(80.75,243.850000000001,31.1713203435596)) ;
#87987=CARTESIAN_POINT('Origin',(80.38,244.220000000001,30.7213203435596)) ;
#87988=CARTESIAN_POINT('',(80.5,244.220000000001,30.7213203435596)) ;
#87989=CARTESIAN_POINT('',(80.38,244.100000000001,30.7213203435596)) ;
#87990=CARTESIAN_POINT('Origin',(80.38,243.950000000001,31.5013203435596)) ;
#87991=CARTESIAN_POINT('',(80.38,243.950000000001,31.6213203435596)) ;
#87992=CARTESIAN_POINT('',(80.5,243.950000000001,31.5013203435596)) ;
#87993=CARTESIAN_POINT('Origin',(79.52,243.980000000001,31.5013203435596)) ;
#87994=CARTESIAN_POINT('',(79.4,243.980000000001,31.5013203435596)) ;
#87995=CARTESIAN_POINT('',(79.28,243.980000000001,31.6213203435596)) ;
#87996=CARTESIAN_POINT('Origin',(79.28,243.980000000001,31.5013203435596)) ;
#87997=CARTESIAN_POINT('',(79.52,244.100000000001,31.5013203435596)) ;
#87998=CARTESIAN_POINT('Origin',(79.52,243.980000000001,31.5013203435596)) ;
#87999=CARTESIAN_POINT('',(79.52,244.220000000001,31.6213203435596)) ;
#88000=CARTESIAN_POINT('Origin',(79.52,244.220000000001,31.5013203435596)) ;
#88001=CARTESIAN_POINT('Origin',(79.52,243.980000000001,31.6213203435596)) ;
#88002=CARTESIAN_POINT('Ctrl Pts',(79.65,243.850000000001,30.9213203435596)) ;
#88003=CARTESIAN_POINT('Ctrl Pts',(79.5168512264577,243.917759673418,30.9213203435596)) ;
#88004=CARTESIAN_POINT('Ctrl Pts',(79.3977344953316,243.978281098255,31.0443420435113)) ;
#88005=CARTESIAN_POINT('Ctrl Pts',(79.4000711137459,243.977093887127,31.1751079336473)) ;
#88006=CARTESIAN_POINT('Ctrl Pts',(79.65,243.850000000001,30.9213203435596)) ;
#88007=CARTESIAN_POINT('Ctrl Pts',(79.5292599996388,243.930168446599,30.9213203435596)) ;
#88008=CARTESIAN_POINT('Ctrl Pts',(79.396519836356,244.015641351745,31.0238212967097)) ;
#88009=CARTESIAN_POINT('Ctrl Pts',(79.3991210649315,244.013966160467,31.1757084683304)) ;
#88010=CARTESIAN_POINT('Ctrl Pts',(79.65,243.850000000001,30.9213203435596)) ;
#88011=CARTESIAN_POINT('Ctrl Pts',(79.5510551013474,243.951963548308,30.9213203435596)) ;
#88012=CARTESIAN_POINT('Ctrl Pts',(79.427258083439,244.081150434729,31.0059874513882)) ;
#88013=CARTESIAN_POINT('Ctrl Pts',(79.4296827587047,244.078620316749,31.1762303714927)) ;
#88014=CARTESIAN_POINT('Ctrl Pts',(79.65,243.850000000001,30.9213203435596)) ;
#88015=CARTESIAN_POINT('Ctrl Pts',(79.5728502030561,243.973758650017,30.9213203435596)) ;
#88016=CARTESIAN_POINT('Ctrl Pts',(79.4934666078253,244.103160830403,31.0290306790137)) ;
#88017=CARTESIAN_POINT('Ctrl Pts',(79.4950227104005,244.100624438084,31.1755560170194)) ;
#88018=CARTESIAN_POINT('Ctrl Pts',(79.65,243.850000000001,30.9213203435596)) ;
#88019=CARTESIAN_POINT('Ctrl Pts',(79.5822365315838,243.983144978544,30.9213203435596)) ;
#88020=CARTESIAN_POINT('Ctrl Pts',(79.5217064362629,244.102266997991,31.0443131728297)) ;
#88021=CARTESIAN_POINT('Ctrl Pts',(79.5228938169118,244.099930276764,31.1751087785408)) ;
#88022=CARTESIAN_POINT('',(79.52,244.100000000001,31.1713203435596)) ;
#88023=CARTESIAN_POINT('',(79.4,243.980000000001,31.1713203435596)) ;
#88024=CARTESIAN_POINT('Origin',(79.52,243.980000000001,31.1713203435596)) ;
#88025=CARTESIAN_POINT('',(79.65,243.850000000001,30.9213203435596)) ;
#88026=CARTESIAN_POINT('Origin',(79.65,243.850000000001,31.1713203435596)) ;
#88027=CARTESIAN_POINT('Origin',(79.65,243.850000000001,31.1713203435596)) ;
#88028=CARTESIAN_POINT('Origin',(79.52,243.980000000001,30.7213203435596)) ;
#88029=CARTESIAN_POINT('',(79.52,244.100000000001,30.7213203435596)) ;
#88030=CARTESIAN_POINT('',(79.4,243.980000000001,30.7213203435596)) ;
#88031=CARTESIAN_POINT('Origin',(80.1,244.220000000001,31.5013203435596)) ;
#88032=CARTESIAN_POINT('',(80.1,244.220000000001,31.6213203435596)) ;
#88033=CARTESIAN_POINT('',(80.1,244.100000000001,31.5013203435596)) ;
#88034=CARTESIAN_POINT('Origin',(79.28,243.650000000001,31.5013203435596)) ;
#88035=CARTESIAN_POINT('',(79.28,243.650000000001,31.6213203435596)) ;
#88036=CARTESIAN_POINT('',(79.4,243.650000000001,31.5013203435596)) ;
#88037=CARTESIAN_POINT('Origin',(80.65,243.380000000001,31.5013203435596)) ;
#88038=CARTESIAN_POINT('',(80.65,243.380000000001,31.6213203435596)) ;
#88039=CARTESIAN_POINT('',(80.65,243.500000000001,31.5013203435596)) ;
#88040=CARTESIAN_POINT('Origin',(80.38,243.100000000001,31.5013203435596)) ;
#88041=CARTESIAN_POINT('',(80.38,243.100000000001,31.6213203435596)) ;
#88042=CARTESIAN_POINT('',(80.5,243.100000000001,31.5013203435596)) ;
#88043=CARTESIAN_POINT('Origin',(80.95,242.280000000001,31.5013203435596)) ;
#88044=CARTESIAN_POINT('',(80.95,242.280000000001,31.6213203435596)) ;
#88045=CARTESIAN_POINT('',(80.95,242.400000000001,31.5013203435596)) ;
#88046=CARTESIAN_POINT('Origin',(81.22,243.650000000001,31.5013203435596)) ;
#88047=CARTESIAN_POINT('',(81.22,243.650000000001,31.6213203435596)) ;
#88048=CARTESIAN_POINT('',(81.1,243.650000000001,31.5013203435596)) ;
#88049=CARTESIAN_POINT('Origin',(81.5,243.380000000001,31.5013203435596)) ;
#88050=CARTESIAN_POINT('',(81.5,243.380000000001,31.6213203435596)) ;
#88051=CARTESIAN_POINT('',(81.5,243.500000000001,31.5013203435596)) ;
#88052=CARTESIAN_POINT('Origin',(82.2,244.100000000001,30.7213203435596)) ;
#88053=CARTESIAN_POINT('',(82.2,243.950000000001,31.1713203435596)) ;
#88054=CARTESIAN_POINT('Origin',(81.1,244.100000000001,30.7213203435596)) ;
#88055=CARTESIAN_POINT('',(80.95,244.100000000001,31.1713203435596)) ;
#88056=CARTESIAN_POINT('Origin',(80.95,243.850000000001,31.1713203435596)) ;
#88057=CARTESIAN_POINT('',(80.95,243.850000000001,30.9213203435596)) ;
#88058=CARTESIAN_POINT('Origin',(81.1,245.200000000001,30.7213203435596)) ;
#88059=CARTESIAN_POINT('',(81.1,244.500000000001,31.1713203435596)) ;
#88060=CARTESIAN_POINT('Origin',(80.85,244.500000000001,31.1713203435596)) ;
#88061=CARTESIAN_POINT('',(80.85,244.500000000001,30.9213203435596)) ;
#88062=CARTESIAN_POINT('Origin',(80.5,245.200000000001,30.7213203435596)) ;
#88063=CARTESIAN_POINT('',(80.65,245.200000000001,31.1713203435596)) ;
#88064=CARTESIAN_POINT('Origin',(80.65,244.950000000001,31.1713203435596)) ;
#88065=CARTESIAN_POINT('',(80.65,244.950000000001,30.9213203435596)) ;
#88066=CARTESIAN_POINT('Origin',(80.5,244.100000000001,30.7213203435596)) ;
#88067=CARTESIAN_POINT('',(80.5,243.950000000001,31.1713203435596)) ;
#88068=CARTESIAN_POINT('Origin',(80.75,243.950000000001,31.1713203435596)) ;
#88069=CARTESIAN_POINT('',(80.75,243.950000000001,30.9213203435596)) ;
#88070=CARTESIAN_POINT('Origin',(79.4,244.100000000001,30.7213203435596)) ;
#88071=CARTESIAN_POINT('',(80.1,244.100000000001,31.1713203435596)) ;
#88072=CARTESIAN_POINT('Origin',(80.1,243.850000000001,31.1713203435596)) ;
#88073=CARTESIAN_POINT('',(80.1,243.850000000001,30.9213203435596)) ;
#88074=CARTESIAN_POINT('Origin',(80.8,243.800000000001,31.6213203435596)) ;
#88075=CARTESIAN_POINT('',(79.05,243.800000000001,31.6213203435596)) ;
#88076=CARTESIAN_POINT('Origin',(80.8,243.800000000001,31.6213203435596)) ;
#88077=CARTESIAN_POINT('Origin',(80.65,243.750000000001,31.1713203435596)) ;
#88078=CARTESIAN_POINT('',(80.65,243.750000000001,30.9213203435596)) ;
#88079=CARTESIAN_POINT('',(80.65,243.500000000001,31.1713203435596)) ;
#88080=CARTESIAN_POINT('Origin',(79.65,243.650000000001,31.1713203435596)) ;
#88081=CARTESIAN_POINT('',(79.65,243.650000000001,30.9213203435596)) ;
#88082=CARTESIAN_POINT('',(79.4,243.650000000001,31.1713203435596)) ;
#88083=CARTESIAN_POINT('Origin',(81.95,243.950000000001,31.1713203435596)) ;
#88084=CARTESIAN_POINT('',(81.95,243.950000000001,30.9213203435596)) ;
#88085=CARTESIAN_POINT('Origin',(81.5,243.750000000001,31.1713203435596)) ;
#88086=CARTESIAN_POINT('',(81.5,243.750000000001,30.9213203435596)) ;
#88087=CARTESIAN_POINT('',(81.5,243.500000000001,31.1713203435596)) ;
#88088=CARTESIAN_POINT('Origin',(80.85,243.650000000001,31.1713203435596)) ;
#88089=CARTESIAN_POINT('',(80.85,243.650000000001,30.9213203435596)) ;
#88090=CARTESIAN_POINT('',(81.1,243.650000000001,31.1713203435596)) ;
#88091=CARTESIAN_POINT('Origin',(80.95,242.650000000001,31.1713203435596)) ;
#88092=CARTESIAN_POINT('',(80.95,242.650000000001,30.9213203435596)) ;
#88093=CARTESIAN_POINT('',(80.95,242.400000000001,31.1713203435596)) ;
#88094=CARTESIAN_POINT('Origin',(80.75,243.100000000001,31.1713203435596)) ;
#88095=CARTESIAN_POINT('',(80.75,243.100000000001,30.9213203435596)) ;
#88096=CARTESIAN_POINT('',(80.5,243.100000000001,31.1713203435596)) ;
#88097=CARTESIAN_POINT('Origin',(82.2,243.500000000001,30.7213203435596)) ;
#88098=CARTESIAN_POINT('Origin',(81.1,243.500000000001,30.7213203435596)) ;
#88099=CARTESIAN_POINT('Origin',(81.1,242.400000000001,30.7213203435596)) ;
#88100=CARTESIAN_POINT('Origin',(80.5,242.400000000001,30.7213203435596)) ;
#88101=CARTESIAN_POINT('Origin',(80.5,243.500000000001,30.7213203435596)) ;
#88102=CARTESIAN_POINT('Origin',(80.8,243.800000000001,30.9213203435596)) ;
#88103=CARTESIAN_POINT('Origin',(80.8,243.800000000001,31.3713203435596)) ;
#88104=CARTESIAN_POINT('',(78.8,243.800000000001,31.3713203435596)) ;
#88105=CARTESIAN_POINT('Origin',(79.05,243.800000000001,31.3713203435596)) ;
#88106=CARTESIAN_POINT('Origin',(80.8,243.800000000001,31.3713203435596)) ;
#88107=CARTESIAN_POINT('Origin',(80.8,243.800000000001,30.7213203435596)) ;
#88108=CARTESIAN_POINT('',(78.8,243.800000000001,30.9713203435596)) ;
#88109=CARTESIAN_POINT('',(78.8,243.800000000001,30.7213203435596)) ;
#88110=CARTESIAN_POINT('',(82.8,243.800000000001,30.9713203435596)) ;
#88111=CARTESIAN_POINT('Origin',(80.8,243.800000000001,30.9713203435596)) ;
#88112=CARTESIAN_POINT('Origin',(80.8,243.800000000001,30.9713203435596)) ;
#88113=CARTESIAN_POINT('Origin',(80.8,243.800000000001,30.9713203435596)) ;
#88114=CARTESIAN_POINT('',(82.55,243.800000000001,30.7213203435596)) ;
#88115=CARTESIAN_POINT('Origin',(80.8,243.800000000001,30.7213203435596)) ;
#88116=CARTESIAN_POINT('Origin',(82.55,243.800000000001,30.9713203435596)) ;
#88117=CARTESIAN_POINT('Origin',(80.8,243.800000000001,30.7213203435596)) ;
#88118=CARTESIAN_POINT('Origin',(79.4,243.500000000001,30.7213203435596)) ;
#117135=UNCERTAINTY_MEASURE_WITH_UNIT(LENGTH_MEASURE(0.01),#117171,
'DISTANCE_ACCURACY_VALUE',
'Maximum model space distance between geometric entities at asserted c
onnectivities') ;
#117147=UNCERTAINTY_MEASURE_WITH_UNIT(LENGTH_MEASURE(0.01),#117171,
'DISTANCE_ACCURACY_VALUE',
'Maximum model space distance between geometric entities at asserted c
onnectivities') ;
#117158=(
GEOMETRIC_REPRESENTATION_CONTEXT(3)
GLOBAL_UNCERTAINTY_ASSIGNED_CONTEXT((#117135))
GLOBAL_UNIT_ASSIGNED_CONTEXT((#117171,#117173,#117174))
REPRESENTATION_CONTEXT('','3D')
) ;
#117170=(
GEOMETRIC_REPRESENTATION_CONTEXT(3)
GLOBAL_UNCERTAINTY_ASSIGNED_CONTEXT((#117147))
GLOBAL_UNIT_ASSIGNED_CONTEXT((#117171,#117173,#117174))
REPRESENTATION_CONTEXT('','3D')
) ;
#117171=(
LENGTH_UNIT()
NAMED_UNIT(*)
SI_UNIT(.MILLI.,.METRE.)
) ;
#117173=(
NAMED_UNIT(*)
PLANE_ANGLE_UNIT()
SI_UNIT($,.RADIAN.)
) ;
#117174=(
NAMED_UNIT(*)
SI_UNIT($,.STERADIAN.)
SOLID_ANGLE_UNIT()
) ;
#117185=SHAPE_DEFINITION_REPRESENTATION(#117207,#117250) ;
#117207=PRODUCT_DEFINITION_SHAPE('',$,#117273) ;
#117250=SHAPE_REPRESENTATION('',(#52017),#117158) ;
#117262=PRODUCT_DEFINITION_CONTEXT('part definition',#117330,'design') ;
#117273=PRODUCT_DEFINITION('Washer_1','Washer_1',#117295,#117262) ;
#117295=PRODUCT_DEFINITION_FORMATION('',$,#117342) ;
#117330=APPLICATION_CONTEXT(
'Core Data for Automotive Mechanical Design Process') ;
#117331=PRODUCT_CONTEXT('part definition',#117330,'mechanical') ;
#117342=PRODUCT('Washer_1','Washer_1',$,(#117331)) ;
#117355=PRESENTATION_STYLE_ASSIGNMENT((#117357)) ;
#117357=SURFACE_STYLE_USAGE(.BOTH.,#117359) ;
#117359=SURFACE_SIDE_STYLE('',(#117361)) ;
#117361=SURFACE_STYLE_FILL_AREA(#117363) ;
#117363=FILL_AREA_STYLE('Opaque(160,160,160)',(#117365)) ;
#117365=FILL_AREA_STYLE_COLOUR('Opaque(160,160,160)',#117367) ;
#117367=COLOUR_RGB('Opaque(160,160,160)', 0.09019608, 0.27058824, 0.51372549) ;
ENDSEC;
END-ISO-10303-21;
